ISO-10303-21;
HEADER;
/* Generated by software containing ST-Developer
 * from STEP Tools, Inc. (www.steptools.com) 
 */

FILE_DESCRIPTION(
/* description */ (''),
/* implementation_level */ '2;1');

FILE_NAME(
/* name */ '01_Coupler_Body_CNC_6061.step',
/* time_stamp */ '2026-10-11T08:53:36-07:00',
/* author */ (''),
/* organization */ (''),
/* preprocessor_version */ 'ST-DEVELOPER v20.2',
/* originating_system */ 'Autodesk Translation Framework v15.15.0.0',
/* authorisation */ '');

FILE_SCHEMA (('AUTOMOTIVE_DESIGN { 1 0 10303 214 3 1 1 }'));
ENDSEC;

DATA;
#10=MECHANICAL_DESIGN_GEOMETRIC_PRESENTATION_REPRESENTATION('',(#72),#3338);
#64=SHAPE_REPRESENTATION_RELATIONSHIP('SRR','None',#3367,#68);
#68=ADVANCED_BREP_SHAPE_REPRESENTATION('',(#76),#3334);
#72=STYLED_ITEM('',(#3436),#76);
#76=MANIFOLD_SOLID_BREP('Body1',#1574);
#80=B_SPLINE_CURVE_WITH_KNOTS('',3,(#2327,#2328,#2329,#2330,#2331,#2332,
#2333,#2334,#2335,#2336),.UNSPECIFIED.,.F.,.F.,(4,2,2,2,4),(0.,0.0466731196164697,
0.0933462392329394,0.146281754847064,0.199217270461189),.UNSPECIFIED.);
#81=B_SPLINE_CURVE_WITH_KNOTS('',3,(#2337,#2338,#2339,#2340,#2341,#2342,
#2343,#2344,#2345,#2346,#2347,#2348,#2349,#2350,#2351,#2352,#2353,#2354,
#2355,#2356,#2357,#2358,#2359,#2360,#2361,#2362,#2363,#2364,#2365,#2366),
 .UNSPECIFIED.,.F.,.F.,(4,2,2,2,2,2,2,2,2,2,2,2,2,2,4),(0.199217270461189,
0.269430202694905,0.339643134928622,0.393818540201201,0.42090624283749,
0.44799394547378,0.475081648110069,0.502169350746359,0.556344756018938,
0.626557688252654,0.696770620486371,0.749706136100495,0.80264165171462,
0.84931477133109,0.895987890947559),.UNSPECIFIED.);
#82=B_SPLINE_CURVE_WITH_KNOTS('',3,(#2389,#2390,#2391,#2392,#2393,#2394,
#2395,#2396,#2397,#2398,#2399,#2400,#2401,#2402,#2403,#2404,#2405,#2406,
#2407,#2408,#2409,#2410,#2411,#2412,#2413,#2414,#2415,#2416,#2417,#2418),
 .UNSPECIFIED.,.F.,.F.,(4,2,2,2,2,2,2,2,2,2,2,2,2,2,4),(0.,0.0466731196164697,
0.0933462392329393,0.146281754847064,0.199217270461189,0.269430202694905,
0.339643134928622,0.393818540201201,0.42090624283749,0.44799394547378,0.475081648110069,
0.502169350746358,0.556344756018937,0.626557688252654,0.69677062048637),
 .UNSPECIFIED.);
#83=B_SPLINE_CURVE_WITH_KNOTS('',3,(#2419,#2420,#2421,#2422,#2423,#2424,
#2425,#2426,#2427,#2428),.UNSPECIFIED.,.F.,.F.,(4,2,2,2,4),(0.69677062048637,
0.749706136100495,0.80264165171462,0.84931477133109,0.895987890947559),
 .UNSPECIFIED.);
#84=B_SPLINE_CURVE_WITH_KNOTS('',3,(#2436,#2437,#2438,#2439,#2440,#2441,
#2442,#2443,#2444,#2445,#2446,#2447),.UNSPECIFIED.,.F.,.F.,(4,2,2,2,2,4),
(0.,0.0270877026362895,0.054175405272579,0.108350810545158,0.178563742778874,
0.248776675012591),.UNSPECIFIED.);
#85=B_SPLINE_CURVE_WITH_KNOTS('',3,(#2448,#2449,#2450,#2451,#2452,#2453,
#2454,#2455,#2456,#2457,#2458,#2459,#2460,#2461,#2462,#2463,#2464,#2465,
#2466,#2467,#2468,#2469,#2470,#2471,#2472,#2473,#2474,#2475),
 .UNSPECIFIED.,.F.,.F.,(4,2,2,2,2,2,2,2,2,2,2,2,2,4),(0.248776675012591,
0.301712190626716,0.35464770624084,0.40132082585731,0.44799394547378,0.494667065090249,
0.541340184706719,0.594275700320844,0.647211215934968,0.717424148168685,
0.787637080402401,0.84181248567498,0.86890018831127,0.895987890947559),
 .UNSPECIFIED.);
#86=B_SPLINE_CURVE_WITH_KNOTS('',3,(#2485,#2486,#2487,#2488,#2489,#2490,
#2491,#2492,#2493,#2494,#2495,#2496,#2497,#2498,#2499,#2500,#2501,#2502,
#2503,#2504,#2505,#2506,#2507,#2508,#2509,#2510,#2511,#2512),
 .UNSPECIFIED.,.F.,.F.,(4,2,2,2,2,2,2,2,2,2,2,2,2,4),(0.,0.0270877026362894,
0.0541754052725788,0.108350810545158,0.178563742778874,0.248776675012591,
0.301712190626716,0.35464770624084,0.40132082585731,0.44799394547378,0.494667065090249,
0.541340184706719,0.594275700320844,0.647211215934968),.UNSPECIFIED.);
#87=B_SPLINE_CURVE_WITH_KNOTS('',3,(#2513,#2514,#2515,#2516,#2517,#2518,
#2519,#2520,#2521,#2522,#2523,#2524),.UNSPECIFIED.,.F.,.F.,(4,2,2,2,2,4),
(0.647211215934968,0.717424148168685,0.787637080402402,0.84181248567498,
0.86890018831127,0.895987890947559),.UNSPECIFIED.);
#88=B_SPLINE_CURVE_WITH_KNOTS('',3,(#2544,#2545,#2546,#2547,#2548,#2549,
#2550,#2551,#2552,#2553,#2554,#2555,#2556,#2557,#2558,#2559,#2560,#2561,
#2562,#2563,#2564,#2565,#2566,#2567,#2568,#2569,#2570,#2571,#2572,#2573,
#2574,#2575,#2576,#2577),.UNSPECIFIED.,.T.,.F.,(4,2,2,2,2,2,2,2,2,2,2,2,
2,2,2,2,4),(0.,0.0471177022580085,0.094235404516017,0.142168460352567,0.190101516189116,
0.237513099195747,0.284924682202378,0.331987109916568,0.379049537630759,
0.426111965344949,0.473174393059139,0.52058597606577,0.567997559072401,
0.615930614908951,0.6638636707455,0.710981373003508,0.758099075261517),
 .UNSPECIFIED.);
#89=B_SPLINE_CURVE_WITH_KNOTS('',3,(#2599,#2600,#2601,#2602,#2603,#2604,
#2605,#2606,#2607,#2608,#2609,#2610,#2611,#2612,#2613,#2614,#2615,#2616,
#2617,#2618,#2619,#2620,#2621,#2622,#2623,#2624,#2625,#2626,#2627,#2628,
#2629,#2630,#2631,#2632),.UNSPECIFIED.,.T.,.F.,(4,2,2,2,2,2,2,2,2,2,2,2,
2,2,2,2,4),(0.,0.0471177022580085,0.094235404516017,0.142168460352567,0.190101516189116,
0.237513099195747,0.284924682202378,0.331987109916568,0.379049537630758,
0.426111965344949,0.473174393059139,0.52058597606577,0.567997559072401,
0.615930614908951,0.6638636707455,0.710981373003509,0.758099075261517),
 .UNSPECIFIED.);
#90=B_SPLINE_CURVE_WITH_KNOTS('',3,(#2639,#2640,#2641,#2642,#2643,#2644,
#2645,#2646,#2647,#2648,#2649,#2650,#2651,#2652,#2653,#2654,#2655,#2656,
#2657,#2658,#2659,#2660,#2661,#2662,#2663,#2664,#2665,#2666,#2667,#2668,
#2669,#2670,#2671,#2672),.UNSPECIFIED.,.T.,.F.,(4,2,2,2,2,2,2,2,2,2,2,2,
2,2,2,2,4),(0.,0.0470624277141901,0.0941248554283803,0.141536438435011,
0.188948021441642,0.236881077278192,0.284814133114742,0.33193183537275,
0.379049537630759,0.426167239888767,0.473284942146776,0.521217997983325,
0.569151053819875,0.616562636826506,0.663974219833137,0.711036647547327,
0.758099075261517),.UNSPECIFIED.);
#91=B_SPLINE_CURVE_WITH_KNOTS('',3,(#2681,#2682,#2683,#2684,#2685,#2686,
#2687,#2688,#2689,#2690,#2691,#2692,#2693,#2694,#2695,#2696,#2697,#2698,
#2699,#2700,#2701,#2702,#2703,#2704,#2705,#2706,#2707,#2708,#2709,#2710,
#2711,#2712,#2713,#2714),.UNSPECIFIED.,.T.,.F.,(4,2,2,2,2,2,2,2,2,2,2,2,
2,2,2,2,4),(0.,0.0470624277141901,0.0941248554283803,0.141536438435011,
0.188948021441642,0.236881077278192,0.284814133114742,0.33193183537275,
0.379049537630759,0.426167239888767,0.473284942146776,0.521217997983325,
0.569151053819875,0.616562636826506,0.663974219833137,0.711036647547327,
0.758099075261517),.UNSPECIFIED.);
#92=B_SPLINE_CURVE_WITH_KNOTS('',3,(#2718,#2719,#2720,#2721,#2722,#2723,
#2724,#2725,#2726,#2727,#2728,#2729),.UNSPECIFIED.,.F.,.F.,(4,2,2,2,2,4),
(0.,0.0270877026362894,0.0541754052725789,0.108350810545158,0.178563742778874,
0.248776675012591),.UNSPECIFIED.);
#93=B_SPLINE_CURVE_WITH_KNOTS('',3,(#2730,#2731,#2732,#2733,#2734,#2735,
#2736,#2737,#2738,#2739,#2740,#2741,#2742,#2743,#2744,#2745,#2746,#2747,
#2748,#2749,#2750,#2751,#2752,#2753,#2754,#2755,#2756,#2757),
 .UNSPECIFIED.,.F.,.F.,(4,2,2,2,2,2,2,2,2,2,2,2,2,4),(0.248776675012591,
0.301712190626716,0.35464770624084,0.40132082585731,0.44799394547378,0.494667065090249,
0.541340184706719,0.594275700320844,0.647211215934968,0.717424148168685,
0.787637080402401,0.84181248567498,0.86890018831127,0.895987890947559),
 .UNSPECIFIED.);
#94=B_SPLINE_CURVE_WITH_KNOTS('',3,(#2761,#2762,#2763,#2764,#2765,#2766,
#2767,#2768,#2769,#2770,#2771,#2772,#2773,#2774,#2775,#2776,#2777,#2778,
#2779,#2780,#2781,#2782,#2783,#2784,#2785,#2786),.UNSPECIFIED.,.F.,.F.,
(4,2,2,2,2,2,2,2,2,2,2,2,4),(0.,0.0471177022580085,0.094235404516017,0.142168460352567,
0.190101516189116,0.237513099195747,0.284924682202378,0.331987109916568,
0.379049537630759,0.426111965344949,0.473174393059139,0.52058597606577,
0.567997559072401),.UNSPECIFIED.);
#95=B_SPLINE_CURVE_WITH_KNOTS('',3,(#2787,#2788,#2789,#2790,#2791,#2792,
#2793,#2794,#2795,#2796),.UNSPECIFIED.,.F.,.F.,(4,2,2,2,4),(0.567997559072401,
0.615930614908951,0.6638636707455,0.710981373003509,0.758099075261517),
 .UNSPECIFIED.);
#96=B_SPLINE_CURVE_WITH_KNOTS('',3,(#2800,#2801,#2802,#2803,#2804,#2805,
#2806,#2807,#2808,#2809),.UNSPECIFIED.,.F.,.F.,(4,2,2,2,4),(0.,0.0471177022580085,
0.094235404516017,0.142168460352567,0.190101516189116),.UNSPECIFIED.);
#97=B_SPLINE_CURVE_WITH_KNOTS('',3,(#2810,#2811,#2812,#2813,#2814,#2815,
#2816,#2817,#2818,#2819,#2820,#2821,#2822,#2823,#2824,#2825,#2826,#2827,
#2828,#2829,#2830,#2831,#2832,#2833,#2834,#2835),.UNSPECIFIED.,.F.,.F.,
(4,2,2,2,2,2,2,2,2,2,2,2,4),(0.190101516189116,0.237513099195747,0.284924682202378,
0.331987109916568,0.379049537630759,0.426111965344949,0.473174393059139,
0.52058597606577,0.567997559072401,0.615930614908951,0.6638636707455,0.710981373003509,
0.758099075261517),.UNSPECIFIED.);
#98=B_SPLINE_CURVE_WITH_KNOTS('',3,(#2839,#2840,#2841,#2842,#2843,#2844,
#2845,#2846,#2847,#2848,#2849,#2850,#2851,#2852,#2853,#2854,#2855,#2856,
#2857,#2858,#2859,#2860,#2861,#2862,#2863,#2864,#2865,#2866),
 .UNSPECIFIED.,.F.,.F.,(4,2,2,2,2,2,2,2,2,2,2,2,2,4),(0.,0.0270877026362895,
0.0541754052725789,0.108350810545158,0.178563742778874,0.248776675012591,
0.301712190626716,0.35464770624084,0.40132082585731,0.44799394547378,0.494667065090249,
0.541340184706719,0.594275700320844,0.647211215934968),.UNSPECIFIED.);
#99=B_SPLINE_CURVE_WITH_KNOTS('',3,(#2867,#2868,#2869,#2870,#2871,#2872,
#2873,#2874,#2875,#2876,#2877,#2878),.UNSPECIFIED.,.F.,.F.,(4,2,2,2,2,4),
(0.647211215934968,0.717424148168685,0.787637080402401,0.84181248567498,
0.86890018831127,0.895987890947559),.UNSPECIFIED.);
#100=B_SPLINE_CURVE_WITH_KNOTS('',3,(#2882,#2883,#2884,#2885,#2886,#2887,
#2888,#2889,#2890,#2891),.UNSPECIFIED.,.F.,.F.,(4,2,2,2,4),(0.,0.0466731196164697,
0.0933462392329394,0.146281754847064,0.199217270461189),.UNSPECIFIED.);
#101=B_SPLINE_CURVE_WITH_KNOTS('',3,(#2892,#2893,#2894,#2895,#2896,#2897,
#2898,#2899,#2900,#2901,#2902,#2903,#2904,#2905,#2906,#2907,#2908,#2909,
#2910,#2911,#2912,#2913,#2914,#2915,#2916,#2917,#2918,#2919,#2920,#2921),
 .UNSPECIFIED.,.F.,.F.,(4,2,2,2,2,2,2,2,2,2,2,2,2,2,4),(0.199217270461189,
0.269430202694905,0.339643134928622,0.393818540201201,0.42090624283749,
0.44799394547378,0.475081648110069,0.502169350746359,0.556344756018938,
0.626557688252654,0.696770620486371,0.749706136100496,0.80264165171462,
0.84931477133109,0.89598789094756),.UNSPECIFIED.);
#102=B_SPLINE_CURVE_WITH_KNOTS('',3,(#2925,#2926,#2927,#2928,#2929,#2930,
#2931,#2932,#2933,#2934,#2935,#2936,#2937,#2938,#2939,#2940,#2941,#2942,
#2943,#2944,#2945,#2946,#2947,#2948,#2949,#2950),.UNSPECIFIED.,.F.,.F.,
(4,2,2,2,2,2,2,2,2,2,2,2,4),(0.,0.0470624277141902,0.0941248554283803,0.141536438435011,
0.188948021441642,0.236881077278192,0.284814133114742,0.33193183537275,
0.379049537630759,0.426167239888767,0.473284942146776,0.521217997983325,
0.569151053819875),.UNSPECIFIED.);
#103=B_SPLINE_CURVE_WITH_KNOTS('',3,(#2951,#2952,#2953,#2954,#2955,#2956,
#2957,#2958,#2959,#2960),.UNSPECIFIED.,.F.,.F.,(4,2,2,2,4),(0.569151053819875,
0.616562636826506,0.663974219833137,0.711036647547327,0.758099075261517),
 .UNSPECIFIED.);
#104=B_SPLINE_CURVE_WITH_KNOTS('',3,(#2964,#2965,#2966,#2967,#2968,#2969,
#2970,#2971,#2972,#2973),.UNSPECIFIED.,.F.,.F.,(4,2,2,2,4),(0.,0.0470624277141902,
0.0941248554283803,0.141536438435011,0.188948021441642),.UNSPECIFIED.);
#105=B_SPLINE_CURVE_WITH_KNOTS('',3,(#2974,#2975,#2976,#2977,#2978,#2979,
#2980,#2981,#2982,#2983,#2984,#2985,#2986,#2987,#2988,#2989,#2990,#2991,
#2992,#2993,#2994,#2995,#2996,#2997,#2998,#2999),.UNSPECIFIED.,.F.,.F.,
(4,2,2,2,2,2,2,2,2,2,2,2,4),(0.188948021441642,0.236881077278192,0.284814133114742,
0.33193183537275,0.379049537630759,0.426167239888767,0.473284942146776,
0.521217997983325,0.569151053819875,0.616562636826506,0.663974219833137,
0.711036647547327,0.758099075261517),.UNSPECIFIED.);
#106=B_SPLINE_CURVE_WITH_KNOTS('',3,(#3003,#3004,#3005,#3006,#3007,#3008,
#3009,#3010,#3011,#3012,#3013,#3014,#3015,#3016,#3017,#3018,#3019,#3020,
#3021,#3022,#3023,#3024,#3025,#3026,#3027,#3028,#3029,#3030,#3031,#3032),
 .UNSPECIFIED.,.F.,.F.,(4,2,2,2,2,2,2,2,2,2,2,2,2,2,4),(0.,0.0466731196164697,
0.0933462392329393,0.146281754847064,0.199217270461189,0.269430202694905,
0.339643134928622,0.393818540201201,0.42090624283749,0.44799394547378,0.475081648110069,
0.502169350746358,0.556344756018937,0.626557688252654,0.69677062048637),
 .UNSPECIFIED.);
#107=B_SPLINE_CURVE_WITH_KNOTS('',3,(#3033,#3034,#3035,#3036,#3037,#3038,
#3039,#3040,#3041,#3042),.UNSPECIFIED.,.F.,.F.,(4,2,2,2,4),(0.69677062048637,
0.749706136100495,0.80264165171462,0.849314771331089,0.895987890947559),
 .UNSPECIFIED.);
#108=CYLINDRICAL_SURFACE('',#1630,1.25);
#109=CYLINDRICAL_SURFACE('',#1636,1.25);
#110=CYLINDRICAL_SURFACE('',#1639,1.25);
#111=CYLINDRICAL_SURFACE('',#1642,1.25);
#112=CYLINDRICAL_SURFACE('',#1648,1.25);
#113=CYLINDRICAL_SURFACE('',#1654,1.25);
#114=CYLINDRICAL_SURFACE('',#1657,1.25);
#115=CYLINDRICAL_SURFACE('',#1660,1.25);
#116=CYLINDRICAL_SURFACE('',#1661,1.25);
#117=CYLINDRICAL_SURFACE('',#1662,1.25);
#118=CYLINDRICAL_SURFACE('',#1663,1.25);
#119=CYLINDRICAL_SURFACE('',#1664,1.25);
#120=CYLINDRICAL_SURFACE('',#1665,3.5);
#121=CYLINDRICAL_SURFACE('',#1669,3.5);
#122=CYLINDRICAL_SURFACE('',#1673,5.025);
#123=CYLINDRICAL_SURFACE('',#1677,5.025);
#124=CYLINDRICAL_SURFACE('',#1721,2.);
#125=CYLINDRICAL_SURFACE('',#1723,21.4);
#126=CYLINDRICAL_SURFACE('',#1725,2.);
#127=CYLINDRICAL_SURFACE('',#1727,2.);
#128=CYLINDRICAL_SURFACE('',#1729,21.4);
#129=CYLINDRICAL_SURFACE('',#1731,2.);
#130=CYLINDRICAL_SURFACE('',#1737,13.5);
#131=CYLINDRICAL_SURFACE('',#1776,2.);
#132=CYLINDRICAL_SURFACE('',#1777,2.);
#133=CYLINDRICAL_SURFACE('',#1778,2.);
#134=CYLINDRICAL_SURFACE('',#1779,2.);
#135=CYLINDRICAL_SURFACE('',#1780,21.4);
#136=CYLINDRICAL_SURFACE('',#1781,21.4);
#139=FACE_BOUND('',#285,.T.);
#140=FACE_BOUND('',#286,.T.);
#141=FACE_BOUND('',#290,.T.);
#142=FACE_BOUND('',#291,.T.);
#143=FACE_BOUND('',#299,.T.);
#144=FACE_BOUND('',#300,.T.);
#145=FACE_BOUND('',#304,.T.);
#146=FACE_BOUND('',#305,.T.);
#147=FACE_BOUND('',#316,.T.);
#148=FACE_BOUND('',#317,.T.);
#149=FACE_BOUND('',#318,.T.);
#150=FACE_BOUND('',#319,.T.);
#151=FACE_BOUND('',#322,.T.);
#152=FACE_BOUND('',#323,.T.);
#153=FACE_BOUND('',#324,.T.);
#154=FACE_BOUND('',#325,.T.);
#155=FACE_BOUND('',#354,.T.);
#156=FACE_BOUND('',#357,.T.);
#157=FACE_BOUND('',#358,.T.);
#158=FACE_BOUND('',#359,.T.);
#159=FACE_BOUND('',#360,.T.);
#160=FACE_BOUND('',#361,.T.);
#161=FACE_BOUND('',#362,.T.);
#162=FACE_BOUND('',#363,.T.);
#163=FACE_BOUND('',#364,.T.);
#164=FACE_BOUND('',#367,.T.);
#165=FACE_BOUND('',#368,.T.);
#166=FACE_BOUND('',#369,.T.);
#167=FACE_BOUND('',#370,.T.);
#168=FACE_BOUND('',#371,.T.);
#169=PLANE('',#1628);
#170=PLANE('',#1634);
#171=PLANE('',#1646);
#172=PLANE('',#1652);
#173=PLANE('',#1668);
#174=PLANE('',#1672);
#175=PLANE('',#1676);
#176=PLANE('',#1680);
#177=PLANE('',#1681);
#178=PLANE('',#1691);
#179=PLANE('',#1701);
#180=PLANE('',#1711);
#181=PLANE('',#1733);
#182=PLANE('',#1741);
#183=PLANE('',#1755);
#184=PLANE('',#1762);
#185=PLANE('',#1769);
#186=PLANE('',#1773);
#191=FACE_OUTER_BOUND('',#283,.T.);
#192=FACE_OUTER_BOUND('',#284,.T.);
#193=FACE_OUTER_BOUND('',#287,.T.);
#194=FACE_OUTER_BOUND('',#288,.T.);
#195=FACE_OUTER_BOUND('',#289,.T.);
#196=FACE_OUTER_BOUND('',#292,.T.);
#197=FACE_OUTER_BOUND('',#293,.T.);
#198=FACE_OUTER_BOUND('',#294,.T.);
#199=FACE_OUTER_BOUND('',#295,.T.);
#200=FACE_OUTER_BOUND('',#296,.T.);
#201=FACE_OUTER_BOUND('',#297,.T.);
#202=FACE_OUTER_BOUND('',#298,.T.);
#203=FACE_OUTER_BOUND('',#301,.T.);
#204=FACE_OUTER_BOUND('',#302,.T.);
#205=FACE_OUTER_BOUND('',#303,.T.);
#206=FACE_OUTER_BOUND('',#306,.T.);
#207=FACE_OUTER_BOUND('',#307,.T.);
#208=FACE_OUTER_BOUND('',#308,.T.);
#209=FACE_OUTER_BOUND('',#309,.T.);
#210=FACE_OUTER_BOUND('',#310,.T.);
#211=FACE_OUTER_BOUND('',#311,.T.);
#212=FACE_OUTER_BOUND('',#312,.T.);
#213=FACE_OUTER_BOUND('',#313,.T.);
#214=FACE_OUTER_BOUND('',#314,.T.);
#215=FACE_OUTER_BOUND('',#315,.T.);
#216=FACE_OUTER_BOUND('',#320,.T.);
#217=FACE_OUTER_BOUND('',#321,.T.);
#218=FACE_OUTER_BOUND('',#326,.T.);
#219=FACE_OUTER_BOUND('',#327,.T.);
#220=FACE_OUTER_BOUND('',#328,.T.);
#221=FACE_OUTER_BOUND('',#329,.T.);
#222=FACE_OUTER_BOUND('',#330,.T.);
#223=FACE_OUTER_BOUND('',#331,.T.);
#224=FACE_OUTER_BOUND('',#332,.T.);
#225=FACE_OUTER_BOUND('',#333,.T.);
#226=FACE_OUTER_BOUND('',#334,.T.);
#227=FACE_OUTER_BOUND('',#335,.T.);
#228=FACE_OUTER_BOUND('',#336,.T.);
#229=FACE_OUTER_BOUND('',#337,.T.);
#230=FACE_OUTER_BOUND('',#338,.T.);
#231=FACE_OUTER_BOUND('',#339,.T.);
#232=FACE_OUTER_BOUND('',#340,.T.);
#233=FACE_OUTER_BOUND('',#341,.T.);
#234=FACE_OUTER_BOUND('',#342,.T.);
#235=FACE_OUTER_BOUND('',#343,.T.);
#236=FACE_OUTER_BOUND('',#344,.T.);
#237=FACE_OUTER_BOUND('',#345,.T.);
#238=FACE_OUTER_BOUND('',#346,.T.);
#239=FACE_OUTER_BOUND('',#347,.T.);
#240=FACE_OUTER_BOUND('',#348,.T.);
#241=FACE_OUTER_BOUND('',#349,.T.);
#242=FACE_OUTER_BOUND('',#350,.T.);
#243=FACE_OUTER_BOUND('',#351,.T.);
#244=FACE_OUTER_BOUND('',#352,.T.);
#245=FACE_OUTER_BOUND('',#353,.T.);
#246=FACE_OUTER_BOUND('',#355,.T.);
#247=FACE_OUTER_BOUND('',#356,.T.);
#248=FACE_OUTER_BOUND('',#365,.T.);
#249=FACE_OUTER_BOUND('',#366,.T.);
#250=FACE_OUTER_BOUND('',#372,.T.);
#251=FACE_OUTER_BOUND('',#373,.T.);
#252=FACE_OUTER_BOUND('',#374,.T.);
#253=FACE_OUTER_BOUND('',#375,.T.);
#254=FACE_OUTER_BOUND('',#376,.T.);
#255=FACE_OUTER_BOUND('',#377,.T.);
#256=FACE_OUTER_BOUND('',#378,.T.);
#257=FACE_OUTER_BOUND('',#379,.T.);
#258=FACE_OUTER_BOUND('',#380,.T.);
#259=FACE_OUTER_BOUND('',#381,.T.);
#260=FACE_OUTER_BOUND('',#382,.T.);
#261=FACE_OUTER_BOUND('',#383,.T.);
#262=FACE_OUTER_BOUND('',#384,.T.);
#263=FACE_OUTER_BOUND('',#385,.T.);
#264=FACE_OUTER_BOUND('',#386,.T.);
#265=FACE_OUTER_BOUND('',#387,.T.);
#266=FACE_OUTER_BOUND('',#388,.T.);
#267=FACE_OUTER_BOUND('',#389,.T.);
#268=FACE_OUTER_BOUND('',#390,.T.);
#269=FACE_OUTER_BOUND('',#391,.T.);
#270=FACE_OUTER_BOUND('',#392,.T.);
#271=FACE_OUTER_BOUND('',#393,.T.);
#283=EDGE_LOOP('',(#1024,#1025,#1026,#1027));
#284=EDGE_LOOP('',(#1028,#1029,#1030,#1031));
#285=EDGE_LOOP('',(#1032));
#286=EDGE_LOOP('',(#1033));
#287=EDGE_LOOP('',(#1034,#1035,#1036,#1037,#1038));
#288=EDGE_LOOP('',(#1039,#1040,#1041,#1042));
#289=EDGE_LOOP('',(#1043,#1044,#1045,#1046));
#290=EDGE_LOOP('',(#1047));
#291=EDGE_LOOP('',(#1048));
#292=EDGE_LOOP('',(#1049,#1050,#1051,#1052,#1053));
#293=EDGE_LOOP('',(#1054,#1055,#1056,#1057));
#294=EDGE_LOOP('',(#1058,#1059,#1060,#1061,#1062));
#295=EDGE_LOOP('',(#1063,#1064,#1065,#1066));
#296=EDGE_LOOP('',(#1067,#1068,#1069,#1070,#1071));
#297=EDGE_LOOP('',(#1072,#1073,#1074,#1075));
#298=EDGE_LOOP('',(#1076,#1077,#1078,#1079));
#299=EDGE_LOOP('',(#1080));
#300=EDGE_LOOP('',(#1081));
#301=EDGE_LOOP('',(#1082,#1083,#1084,#1085));
#302=EDGE_LOOP('',(#1086,#1087,#1088,#1089));
#303=EDGE_LOOP('',(#1090,#1091,#1092,#1093));
#304=EDGE_LOOP('',(#1094));
#305=EDGE_LOOP('',(#1095));
#306=EDGE_LOOP('',(#1096,#1097,#1098,#1099));
#307=EDGE_LOOP('',(#1100,#1101,#1102,#1103));
#308=EDGE_LOOP('',(#1104,#1105,#1106,#1107));
#309=EDGE_LOOP('',(#1108,#1109,#1110,#1111));
#310=EDGE_LOOP('',(#1112,#1113,#1114,#1115));
#311=EDGE_LOOP('',(#1116,#1117,#1118,#1119,#1120,#1121));
#312=EDGE_LOOP('',(#1122,#1123,#1124,#1125,#1126,#1127));
#313=EDGE_LOOP('',(#1128,#1129,#1130,#1131,#1132,#1133));
#314=EDGE_LOOP('',(#1134,#1135,#1136,#1137,#1138,#1139));
#315=EDGE_LOOP('',(#1140,#1141,#1142,#1143));
#316=EDGE_LOOP('',(#1144,#1145));
#317=EDGE_LOOP('',(#1146,#1147));
#318=EDGE_LOOP('',(#1148,#1149));
#319=EDGE_LOOP('',(#1150,#1151));
#320=EDGE_LOOP('',(#1152));
#321=EDGE_LOOP('',(#1153,#1154,#1155,#1156));
#322=EDGE_LOOP('',(#1157,#1158));
#323=EDGE_LOOP('',(#1159,#1160));
#324=EDGE_LOOP('',(#1161,#1162));
#325=EDGE_LOOP('',(#1163,#1164));
#326=EDGE_LOOP('',(#1165));
#327=EDGE_LOOP('',(#1166,#1167,#1168,#1169));
#328=EDGE_LOOP('',(#1170));
#329=EDGE_LOOP('',(#1171,#1172,#1173,#1174));
#330=EDGE_LOOP('',(#1175));
#331=EDGE_LOOP('',(#1176,#1177,#1178,#1179));
#332=EDGE_LOOP('',(#1180,#1181,#1182,#1183));
#333=EDGE_LOOP('',(#1184,#1185,#1186,#1187));
#334=EDGE_LOOP('',(#1188,#1189,#1190,#1191));
#335=EDGE_LOOP('',(#1192,#1193,#1194,#1195));
#336=EDGE_LOOP('',(#1196,#1197,#1198,#1199));
#337=EDGE_LOOP('',(#1200,#1201,#1202,#1203));
#338=EDGE_LOOP('',(#1204,#1205,#1206,#1207));
#339=EDGE_LOOP('',(#1208,#1209,#1210,#1211));
#340=EDGE_LOOP('',(#1212,#1213,#1214,#1215));
#341=EDGE_LOOP('',(#1216,#1217,#1218,#1219));
#342=EDGE_LOOP('',(#1220,#1221,#1222,#1223));
#343=EDGE_LOOP('',(#1224,#1225,#1226,#1227));
#344=EDGE_LOOP('',(#1228,#1229,#1230,#1231));
#345=EDGE_LOOP('',(#1232,#1233,#1234,#1235));
#346=EDGE_LOOP('',(#1236,#1237,#1238,#1239));
#347=EDGE_LOOP('',(#1240,#1241,#1242,#1243));
#348=EDGE_LOOP('',(#1244,#1245,#1246,#1247));
#349=EDGE_LOOP('',(#1248,#1249,#1250,#1251));
#350=EDGE_LOOP('',(#1252,#1253,#1254,#1255));
#351=EDGE_LOOP('',(#1256,#1257,#1258,#1259));
#352=EDGE_LOOP('',(#1260,#1261,#1262,#1263));
#353=EDGE_LOOP('',(#1264,#1265,#1266,#1267,#1268,#1269,#1270,#1271,#1272,
#1273,#1274,#1275,#1276,#1277,#1278,#1279));
#354=EDGE_LOOP('',(#1280));
#355=EDGE_LOOP('',(#1281,#1282,#1283,#1284));
#356=EDGE_LOOP('',(#1285,#1286,#1287,#1288));
#357=EDGE_LOOP('',(#1289));
#358=EDGE_LOOP('',(#1290));
#359=EDGE_LOOP('',(#1291));
#360=EDGE_LOOP('',(#1292));
#361=EDGE_LOOP('',(#1293,#1294));
#362=EDGE_LOOP('',(#1295,#1296));
#363=EDGE_LOOP('',(#1297,#1298));
#364=EDGE_LOOP('',(#1299,#1300));
#365=EDGE_LOOP('',(#1301,#1302,#1303,#1304));
#366=EDGE_LOOP('',(#1305,#1306,#1307,#1308,#1309,#1310,#1311,#1312,#1313,
#1314,#1315,#1316,#1317,#1318,#1319,#1320));
#367=EDGE_LOOP('',(#1321));
#368=EDGE_LOOP('',(#1322));
#369=EDGE_LOOP('',(#1323));
#370=EDGE_LOOP('',(#1324));
#371=EDGE_LOOP('',(#1325));
#372=EDGE_LOOP('',(#1326,#1327,#1328,#1329));
#373=EDGE_LOOP('',(#1330,#1331,#1332,#1333));
#374=EDGE_LOOP('',(#1334,#1335,#1336,#1337));
#375=EDGE_LOOP('',(#1338,#1339,#1340,#1341));
#376=EDGE_LOOP('',(#1342,#1343,#1344,#1345));
#377=EDGE_LOOP('',(#1346,#1347,#1348,#1349));
#378=EDGE_LOOP('',(#1350,#1351,#1352,#1353));
#379=EDGE_LOOP('',(#1354,#1355,#1356,#1357));
#380=EDGE_LOOP('',(#1358,#1359,#1360,#1361));
#381=EDGE_LOOP('',(#1362,#1363,#1364,#1365));
#382=EDGE_LOOP('',(#1366,#1367,#1368,#1369));
#383=EDGE_LOOP('',(#1370,#1371,#1372,#1373));
#384=EDGE_LOOP('',(#1374,#1375,#1376,#1377));
#385=EDGE_LOOP('',(#1378,#1379,#1380,#1381));
#386=EDGE_LOOP('',(#1382,#1383,#1384,#1385));
#387=EDGE_LOOP('',(#1386,#1387,#1388,#1389));
#388=EDGE_LOOP('',(#1390,#1391,#1392,#1393));
#389=EDGE_LOOP('',(#1394,#1395,#1396,#1397));
#390=EDGE_LOOP('',(#1398,#1399,#1400,#1401));
#391=EDGE_LOOP('',(#1402,#1403,#1404,#1405));
#392=EDGE_LOOP('',(#1406,#1407,#1408,#1409));
#393=EDGE_LOOP('',(#1410,#1411,#1412,#1413));
#405=LINE('',#2311,#502);
#406=LINE('',#2316,#503);
#407=LINE('',#2318,#504);
#408=LINE('',#2320,#505);
#409=LINE('',#2321,#506);
#410=LINE('',#2367,#507);
#411=LINE('',#2372,#508);
#412=LINE('',#2377,#509);
#413=LINE('',#2379,#510);
#414=LINE('',#2381,#511);
#415=LINE('',#2382,#512);
#416=LINE('',#2387,#513);
#417=LINE('',#2431,#514);
#418=LINE('',#2476,#515);
#419=LINE('',#2479,#516);
#420=LINE('',#2483,#517);
#421=LINE('',#2529,#518);
#422=LINE('',#2534,#519);
#423=LINE('',#2536,#520);
#424=LINE('',#2538,#521);
#425=LINE('',#2539,#522);
#426=LINE('',#2578,#523);
#427=LINE('',#2583,#524);
#428=LINE('',#2588,#525);
#429=LINE('',#2590,#526);
#430=LINE('',#2592,#527);
#431=LINE('',#2593,#528);
#432=LINE('',#2598,#529);
#433=LINE('',#2635,#530);
#434=LINE('',#2673,#531);
#435=LINE('',#2676,#532);
#436=LINE('',#2680,#533);
#437=LINE('',#2759,#534);
#438=LINE('',#2837,#535);
#439=LINE('',#2923,#536);
#440=LINE('',#3001,#537);
#441=LINE('',#3047,#538);
#442=LINE('',#3054,#539);
#443=LINE('',#3061,#540);
#444=LINE('',#3068,#541);
#445=LINE('',#3073,#542);
#446=LINE('',#3075,#543);
#447=LINE('',#3076,#544);
#448=LINE('',#3080,#545);
#449=LINE('',#3087,#546);
#450=LINE('',#3091,#547);
#451=LINE('',#3096,#548);
#452=LINE('',#3097,#549);
#453=LINE('',#3101,#550);
#454=LINE('',#3108,#551);
#455=LINE('',#3112,#552);
#456=LINE('',#3117,#553);
#457=LINE('',#3118,#554);
#458=LINE('',#3122,#555);
#459=LINE('',#3129,#556);
#460=LINE('',#3133,#557);
#461=LINE('',#3138,#558);
#462=LINE('',#3139,#559);
#463=LINE('',#3143,#560);
#464=LINE('',#3150,#561);
#465=LINE('',#3157,#562);
#466=LINE('',#3161,#563);
#467=LINE('',#3167,#564);
#468=LINE('',#3171,#565);
#469=LINE('',#3181,#566);
#470=LINE('',#3185,#567);
#471=LINE('',#3189,#568);
#472=LINE('',#3199,#569);
#473=LINE('',#3207,#570);
#474=LINE('',#3215,#571);
#475=LINE('',#3222,#572);
#476=LINE('',#3224,#573);
#477=LINE('',#3225,#574);
#478=LINE('',#3227,#575);
#479=LINE('',#3230,#576);
#480=LINE('',#3234,#577);
#481=LINE('',#3237,#578);
#482=LINE('',#3240,#579);
#483=LINE('',#3243,#580);
#484=LINE('',#3247,#581);
#485=LINE('',#3250,#582);
#486=LINE('',#3253,#583);
#487=LINE('',#3255,#584);
#488=LINE('',#3257,#585);
#489=LINE('',#3259,#586);
#490=LINE('',#3261,#587);
#491=LINE('',#3263,#588);
#492=LINE('',#3266,#589);
#493=LINE('',#3268,#590);
#494=LINE('',#3270,#591);
#495=LINE('',#3272,#592);
#502=VECTOR('',#1826,1.35);
#503=VECTOR('',#1831,10.);
#504=VECTOR('',#1832,10.);
#505=VECTOR('',#1833,10.);
#506=VECTOR('',#1834,10.);
#507=VECTOR('',#1839,1.25);
#508=VECTOR('',#1844,1.35);
#509=VECTOR('',#1849,10.);
#510=VECTOR('',#1850,10.);
#511=VECTOR('',#1851,10.);
#512=VECTOR('',#1852,10.);
#513=VECTOR('',#1857,1.25);
#514=VECTOR('',#1860,1.35);
#515=VECTOR('',#1865,1.25);
#516=VECTOR('',#1868,1.35);
#517=VECTOR('',#1873,1.25);
#518=VECTOR('',#1878,1.35);
#519=VECTOR('',#1883,10.);
#520=VECTOR('',#1884,10.);
#521=VECTOR('',#1885,10.);
#522=VECTOR('',#1886,10.);
#523=VECTOR('',#1891,1.25);
#524=VECTOR('',#1896,1.35);
#525=VECTOR('',#1901,10.);
#526=VECTOR('',#1902,10.);
#527=VECTOR('',#1903,10.);
#528=VECTOR('',#1904,10.);
#529=VECTOR('',#1909,1.25);
#530=VECTOR('',#1912,1.35);
#531=VECTOR('',#1917,1.25);
#532=VECTOR('',#1920,1.35);
#533=VECTOR('',#1925,1.25);
#534=VECTOR('',#1928,1.25);
#535=VECTOR('',#1931,1.25);
#536=VECTOR('',#1934,1.25);
#537=VECTOR('',#1937,1.25);
#538=VECTOR('',#1942,3.5);
#539=VECTOR('',#1951,3.5);
#540=VECTOR('',#1960,5.025);
#541=VECTOR('',#1969,5.025);
#542=VECTOR('',#1976,10.);
#543=VECTOR('',#1977,10.);
#544=VECTOR('',#1978,10.);
#545=VECTOR('',#1981,10.);
#546=VECTOR('',#1990,10.);
#547=VECTOR('',#1995,10.);
#548=VECTOR('',#2002,10.);
#549=VECTOR('',#2003,10.);
#550=VECTOR('',#2006,10.);
#551=VECTOR('',#2015,10.);
#552=VECTOR('',#2020,10.);
#553=VECTOR('',#2027,10.);
#554=VECTOR('',#2028,10.);
#555=VECTOR('',#2031,10.);
#556=VECTOR('',#2040,10.);
#557=VECTOR('',#2045,10.);
#558=VECTOR('',#2052,10.);
#559=VECTOR('',#2053,10.);
#560=VECTOR('',#2056,10.);
#561=VECTOR('',#2065,10.);
#562=VECTOR('',#2076,10.);
#563=VECTOR('',#2081,10.);
#564=VECTOR('',#2090,10.);
#565=VECTOR('',#2095,10.);
#566=VECTOR('',#2110,13.7);
#567=VECTOR('',#2115,13.5);
#568=VECTOR('',#2120,13.9);
#569=VECTOR('',#2129,10.);
#570=VECTOR('',#2136,10.);
#571=VECTOR('',#2143,10.);
#572=VECTOR('',#2150,10.);
#573=VECTOR('',#2153,10.);
#574=VECTOR('',#2154,10.);
#575=VECTOR('',#2157,10.);
#576=VECTOR('',#2160,10.);
#577=VECTOR('',#2165,10.);
#578=VECTOR('',#2170,10.);
#579=VECTOR('',#2175,10.);
#580=VECTOR('',#2178,10.);
#581=VECTOR('',#2183,10.);
#582=VECTOR('',#2188,10.);
#583=VECTOR('',#2193,10.);
#584=VECTOR('',#2196,10.);
#585=VECTOR('',#2199,10.);
#586=VECTOR('',#2202,10.);
#587=VECTOR('',#2205,10.);
#588=VECTOR('',#2208,10.);
#589=VECTOR('',#2213,10.);
#590=VECTOR('',#2216,10.);
#591=VECTOR('',#2219,10.);
#592=VECTOR('',#2222,10.);
#599=CIRCLE('',#1626,1.45);
#600=CIRCLE('',#1627,1.25);
#601=CIRCLE('',#1629,1.45);
#602=CIRCLE('',#1632,1.45);
#603=CIRCLE('',#1633,1.25);
#604=CIRCLE('',#1635,1.45);
#605=CIRCLE('',#1638,1.25);
#606=CIRCLE('',#1641,1.25);
#607=CIRCLE('',#1644,1.45);
#608=CIRCLE('',#1645,1.25);
#609=CIRCLE('',#1647,1.45);
#610=CIRCLE('',#1650,1.45);
#611=CIRCLE('',#1651,1.25);
#612=CIRCLE('',#1653,1.45);
#613=CIRCLE('',#1656,1.25);
#614=CIRCLE('',#1659,1.25);
#615=CIRCLE('',#1666,3.5);
#616=CIRCLE('',#1667,3.5);
#617=CIRCLE('',#1670,3.5);
#618=CIRCLE('',#1671,3.5);
#619=CIRCLE('',#1674,5.025);
#620=CIRCLE('',#1675,5.025);
#621=CIRCLE('',#1678,5.025);
#622=CIRCLE('',#1679,5.025);
#623=CIRCLE('',#1683,2.);
#624=CIRCLE('',#1684,1.6);
#625=CIRCLE('',#1686,21.8);
#626=CIRCLE('',#1687,21.4);
#627=CIRCLE('',#1689,2.);
#628=CIRCLE('',#1690,1.6);
#629=CIRCLE('',#1693,2.);
#630=CIRCLE('',#1694,1.6);
#631=CIRCLE('',#1696,21.8);
#632=CIRCLE('',#1697,21.4);
#633=CIRCLE('',#1699,2.);
#634=CIRCLE('',#1700,1.6);
#635=CIRCLE('',#1703,2.);
#636=CIRCLE('',#1704,1.6);
#637=CIRCLE('',#1706,21.8);
#638=CIRCLE('',#1707,21.4);
#639=CIRCLE('',#1709,2.);
#640=CIRCLE('',#1710,1.6);
#641=CIRCLE('',#1713,2.);
#642=CIRCLE('',#1714,1.6);
#643=CIRCLE('',#1716,21.8);
#644=CIRCLE('',#1717,21.4);
#645=CIRCLE('',#1719,2.);
#646=CIRCLE('',#1720,1.6);
#647=CIRCLE('',#1722,2.);
#648=CIRCLE('',#1724,21.4);
#649=CIRCLE('',#1726,2.);
#650=CIRCLE('',#1728,2.);
#651=CIRCLE('',#1730,21.4);
#652=CIRCLE('',#1732,2.);
#653=CIRCLE('',#1734,13.9);
#654=CIRCLE('',#1736,13.5);
#655=CIRCLE('',#1738,13.5);
#656=CIRCLE('',#1740,14.3);
#657=CIRCLE('',#1742,1.2);
#658=CIRCLE('',#1743,22.2);
#659=CIRCLE('',#1744,1.2);
#660=CIRCLE('',#1745,1.2);
#661=CIRCLE('',#1746,22.2);
#662=CIRCLE('',#1747,1.2);
#663=CIRCLE('',#1748,1.2);
#664=CIRCLE('',#1749,22.2);
#665=CIRCLE('',#1750,1.2);
#666=CIRCLE('',#1751,1.2);
#667=CIRCLE('',#1752,22.2);
#668=CIRCLE('',#1753,1.2);
#669=CIRCLE('',#1757,2.);
#670=CIRCLE('',#1759,21.4);
#671=CIRCLE('',#1761,2.);
#672=CIRCLE('',#1764,2.);
#673=CIRCLE('',#1766,21.4);
#674=CIRCLE('',#1768,2.);
#684=VERTEX_POINT('',#2308);
#685=VERTEX_POINT('',#2310);
#686=VERTEX_POINT('',#2314);
#687=VERTEX_POINT('',#2315);
#688=VERTEX_POINT('',#2317);
#689=VERTEX_POINT('',#2319);
#690=VERTEX_POINT('',#2322);
#691=VERTEX_POINT('',#2325);
#692=VERTEX_POINT('',#2326);
#693=VERTEX_POINT('',#2369);
#694=VERTEX_POINT('',#2371);
#695=VERTEX_POINT('',#2375);
#696=VERTEX_POINT('',#2376);
#697=VERTEX_POINT('',#2378);
#698=VERTEX_POINT('',#2380);
#699=VERTEX_POINT('',#2383);
#700=VERTEX_POINT('',#2386);
#701=VERTEX_POINT('',#2388);
#702=VERTEX_POINT('',#2430);
#703=VERTEX_POINT('',#2434);
#704=VERTEX_POINT('',#2435);
#705=VERTEX_POINT('',#2478);
#706=VERTEX_POINT('',#2482);
#707=VERTEX_POINT('',#2484);
#708=VERTEX_POINT('',#2526);
#709=VERTEX_POINT('',#2528);
#710=VERTEX_POINT('',#2532);
#711=VERTEX_POINT('',#2533);
#712=VERTEX_POINT('',#2535);
#713=VERTEX_POINT('',#2537);
#714=VERTEX_POINT('',#2540);
#715=VERTEX_POINT('',#2543);
#716=VERTEX_POINT('',#2580);
#717=VERTEX_POINT('',#2582);
#718=VERTEX_POINT('',#2586);
#719=VERTEX_POINT('',#2587);
#720=VERTEX_POINT('',#2589);
#721=VERTEX_POINT('',#2591);
#722=VERTEX_POINT('',#2594);
#723=VERTEX_POINT('',#2597);
#724=VERTEX_POINT('',#2634);
#725=VERTEX_POINT('',#2638);
#726=VERTEX_POINT('',#2675);
#727=VERTEX_POINT('',#2679);
#728=VERTEX_POINT('',#2716);
#729=VERTEX_POINT('',#2717);
#730=VERTEX_POINT('',#2758);
#731=VERTEX_POINT('',#2760);
#732=VERTEX_POINT('',#2798);
#733=VERTEX_POINT('',#2799);
#734=VERTEX_POINT('',#2836);
#735=VERTEX_POINT('',#2838);
#736=VERTEX_POINT('',#2880);
#737=VERTEX_POINT('',#2881);
#738=VERTEX_POINT('',#2922);
#739=VERTEX_POINT('',#2924);
#740=VERTEX_POINT('',#2962);
#741=VERTEX_POINT('',#2963);
#742=VERTEX_POINT('',#3000);
#743=VERTEX_POINT('',#3002);
#744=VERTEX_POINT('',#3044);
#745=VERTEX_POINT('',#3046);
#746=VERTEX_POINT('',#3051);
#747=VERTEX_POINT('',#3053);
#748=VERTEX_POINT('',#3058);
#749=VERTEX_POINT('',#3060);
#750=VERTEX_POINT('',#3065);
#751=VERTEX_POINT('',#3067);
#752=VERTEX_POINT('',#3072);
#753=VERTEX_POINT('',#3074);
#754=VERTEX_POINT('',#3078);
#755=VERTEX_POINT('',#3079);
#756=VERTEX_POINT('',#3084);
#757=VERTEX_POINT('',#3086);
#758=VERTEX_POINT('',#3090);
#759=VERTEX_POINT('',#3095);
#760=VERTEX_POINT('',#3099);
#761=VERTEX_POINT('',#3100);
#762=VERTEX_POINT('',#3105);
#763=VERTEX_POINT('',#3107);
#764=VERTEX_POINT('',#3111);
#765=VERTEX_POINT('',#3116);
#766=VERTEX_POINT('',#3120);
#767=VERTEX_POINT('',#3121);
#768=VERTEX_POINT('',#3126);
#769=VERTEX_POINT('',#3128);
#770=VERTEX_POINT('',#3132);
#771=VERTEX_POINT('',#3137);
#772=VERTEX_POINT('',#3141);
#773=VERTEX_POINT('',#3142);
#774=VERTEX_POINT('',#3147);
#775=VERTEX_POINT('',#3149);
#776=VERTEX_POINT('',#3156);
#777=VERTEX_POINT('',#3160);
#778=VERTEX_POINT('',#3166);
#779=VERTEX_POINT('',#3170);
#780=VERTEX_POINT('',#3176);
#781=VERTEX_POINT('',#3179);
#782=VERTEX_POINT('',#3183);
#783=VERTEX_POINT('',#3187);
#784=VERTEX_POINT('',#3191);
#785=VERTEX_POINT('',#3192);
#786=VERTEX_POINT('',#3194);
#787=VERTEX_POINT('',#3196);
#788=VERTEX_POINT('',#3198);
#789=VERTEX_POINT('',#3200);
#790=VERTEX_POINT('',#3202);
#791=VERTEX_POINT('',#3204);
#792=VERTEX_POINT('',#3206);
#793=VERTEX_POINT('',#3208);
#794=VERTEX_POINT('',#3210);
#795=VERTEX_POINT('',#3212);
#796=VERTEX_POINT('',#3214);
#797=VERTEX_POINT('',#3216);
#798=VERTEX_POINT('',#3218);
#799=VERTEX_POINT('',#3220);
#800=VERTEX_POINT('',#3229);
#801=VERTEX_POINT('',#3233);
#802=VERTEX_POINT('',#3242);
#803=VERTEX_POINT('',#3246);
#814=EDGE_CURVE('',#684,#684,#599,.T.);
#815=EDGE_CURVE('',#684,#685,#405,.T.);
#816=EDGE_CURVE('',#685,#685,#600,.T.);
#817=EDGE_CURVE('',#686,#687,#406,.T.);
#818=EDGE_CURVE('',#688,#686,#407,.T.);
#819=EDGE_CURVE('',#689,#688,#408,.T.);
#820=EDGE_CURVE('',#687,#689,#409,.T.);
#821=EDGE_CURVE('',#690,#690,#601,.T.);
#822=EDGE_CURVE('',#691,#692,#80,.T.);
#823=EDGE_CURVE('',#692,#691,#81,.T.);
#824=EDGE_CURVE('',#692,#685,#410,.T.);
#825=EDGE_CURVE('',#693,#693,#602,.T.);
#826=EDGE_CURVE('',#693,#694,#411,.T.);
#827=EDGE_CURVE('',#694,#694,#603,.T.);
#828=EDGE_CURVE('',#695,#696,#412,.T.);
#829=EDGE_CURVE('',#697,#695,#413,.T.);
#830=EDGE_CURVE('',#698,#697,#414,.T.);
#831=EDGE_CURVE('',#696,#698,#415,.T.);
#832=EDGE_CURVE('',#699,#699,#604,.T.);
#833=EDGE_CURVE('',#694,#700,#416,.T.);
#834=EDGE_CURVE('',#701,#700,#82,.T.);
#835=EDGE_CURVE('',#700,#701,#83,.T.);
#836=EDGE_CURVE('',#690,#702,#417,.T.);
#837=EDGE_CURVE('',#702,#702,#605,.T.);
#838=EDGE_CURVE('',#703,#704,#84,.T.);
#839=EDGE_CURVE('',#704,#703,#85,.T.);
#840=EDGE_CURVE('',#704,#702,#418,.T.);
#841=EDGE_CURVE('',#699,#705,#419,.T.);
#842=EDGE_CURVE('',#705,#705,#606,.T.);
#843=EDGE_CURVE('',#705,#706,#420,.T.);
#844=EDGE_CURVE('',#707,#706,#86,.T.);
#845=EDGE_CURVE('',#706,#707,#87,.T.);
#846=EDGE_CURVE('',#708,#708,#607,.T.);
#847=EDGE_CURVE('',#708,#709,#421,.T.);
#848=EDGE_CURVE('',#709,#709,#608,.T.);
#849=EDGE_CURVE('',#710,#711,#422,.T.);
#850=EDGE_CURVE('',#712,#710,#423,.T.);
#851=EDGE_CURVE('',#713,#712,#424,.T.);
#852=EDGE_CURVE('',#711,#713,#425,.T.);
#853=EDGE_CURVE('',#714,#714,#609,.T.);
#854=EDGE_CURVE('',#715,#715,#88,.T.);
#855=EDGE_CURVE('',#715,#709,#426,.T.);
#856=EDGE_CURVE('',#716,#716,#610,.T.);
#857=EDGE_CURVE('',#716,#717,#427,.T.);
#858=EDGE_CURVE('',#717,#717,#611,.T.);
#859=EDGE_CURVE('',#718,#719,#428,.T.);
#860=EDGE_CURVE('',#720,#718,#429,.T.);
#861=EDGE_CURVE('',#721,#720,#430,.T.);
#862=EDGE_CURVE('',#719,#721,#431,.T.);
#863=EDGE_CURVE('',#722,#722,#612,.T.);
#864=EDGE_CURVE('',#717,#723,#432,.T.);
#865=EDGE_CURVE('',#723,#723,#89,.T.);
#866=EDGE_CURVE('',#714,#724,#433,.T.);
#867=EDGE_CURVE('',#724,#724,#613,.T.);
#868=EDGE_CURVE('',#725,#725,#90,.T.);
#869=EDGE_CURVE('',#725,#724,#434,.T.);
#870=EDGE_CURVE('',#722,#726,#435,.T.);
#871=EDGE_CURVE('',#726,#726,#614,.T.);
#872=EDGE_CURVE('',#726,#727,#436,.T.);
#873=EDGE_CURVE('',#727,#727,#91,.T.);
#874=EDGE_CURVE('',#728,#729,#92,.T.);
#875=EDGE_CURVE('',#729,#728,#93,.T.);
#876=EDGE_CURVE('',#729,#730,#437,.T.);
#877=EDGE_CURVE('',#731,#730,#94,.T.);
#878=EDGE_CURVE('',#730,#731,#95,.T.);
#879=EDGE_CURVE('',#732,#733,#96,.T.);
#880=EDGE_CURVE('',#733,#732,#97,.T.);
#881=EDGE_CURVE('',#733,#734,#438,.T.);
#882=EDGE_CURVE('',#735,#734,#98,.T.);
#883=EDGE_CURVE('',#734,#735,#99,.T.);
#884=EDGE_CURVE('',#736,#737,#100,.T.);
#885=EDGE_CURVE('',#737,#736,#101,.T.);
#886=EDGE_CURVE('',#737,#738,#439,.T.);
#887=EDGE_CURVE('',#739,#738,#102,.T.);
#888=EDGE_CURVE('',#738,#739,#103,.T.);
#889=EDGE_CURVE('',#740,#741,#104,.T.);
#890=EDGE_CURVE('',#741,#740,#105,.T.);
#891=EDGE_CURVE('',#741,#742,#440,.T.);
#892=EDGE_CURVE('',#743,#742,#106,.T.);
#893=EDGE_CURVE('',#742,#743,#107,.T.);
#894=EDGE_CURVE('',#744,#744,#615,.T.);
#895=EDGE_CURVE('',#744,#745,#441,.T.);
#896=EDGE_CURVE('',#745,#745,#616,.T.);
#897=EDGE_CURVE('',#746,#746,#617,.T.);
#898=EDGE_CURVE('',#746,#747,#442,.T.);
#899=EDGE_CURVE('',#747,#747,#618,.T.);
#900=EDGE_CURVE('',#748,#748,#619,.T.);
#901=EDGE_CURVE('',#748,#749,#443,.T.);
#902=EDGE_CURVE('',#749,#749,#620,.T.);
#903=EDGE_CURVE('',#750,#750,#621,.T.);
#904=EDGE_CURVE('',#750,#751,#444,.T.);
#905=EDGE_CURVE('',#751,#751,#622,.T.);
#906=EDGE_CURVE('',#752,#718,#445,.T.);
#907=EDGE_CURVE('',#719,#753,#446,.T.);
#908=EDGE_CURVE('',#753,#752,#447,.T.);
#909=EDGE_CURVE('',#754,#755,#448,.T.);
#910=EDGE_CURVE('',#755,#718,#623,.T.);
#911=EDGE_CURVE('',#752,#754,#624,.T.);
#912=EDGE_CURVE('',#754,#756,#625,.T.);
#913=EDGE_CURVE('',#756,#757,#449,.T.);
#914=EDGE_CURVE('',#757,#755,#626,.T.);
#915=EDGE_CURVE('',#758,#687,#450,.T.);
#916=EDGE_CURVE('',#687,#757,#627,.T.);
#917=EDGE_CURVE('',#756,#758,#628,.T.);
#918=EDGE_CURVE('',#759,#686,#451,.T.);
#919=EDGE_CURVE('',#758,#759,#452,.T.);
#920=EDGE_CURVE('',#760,#761,#453,.T.);
#921=EDGE_CURVE('',#761,#686,#629,.T.);
#922=EDGE_CURVE('',#759,#760,#630,.T.);
#923=EDGE_CURVE('',#760,#762,#631,.T.);
#924=EDGE_CURVE('',#762,#763,#454,.T.);
#925=EDGE_CURVE('',#763,#761,#632,.T.);
#926=EDGE_CURVE('',#764,#711,#455,.T.);
#927=EDGE_CURVE('',#711,#763,#633,.T.);
#928=EDGE_CURVE('',#762,#764,#634,.T.);
#929=EDGE_CURVE('',#765,#710,#456,.T.);
#930=EDGE_CURVE('',#764,#765,#457,.T.);
#931=EDGE_CURVE('',#766,#767,#458,.T.);
#932=EDGE_CURVE('',#767,#710,#635,.T.);
#933=EDGE_CURVE('',#765,#766,#636,.T.);
#934=EDGE_CURVE('',#766,#768,#637,.T.);
#935=EDGE_CURVE('',#768,#769,#459,.T.);
#936=EDGE_CURVE('',#769,#767,#638,.T.);
#937=EDGE_CURVE('',#770,#696,#460,.T.);
#938=EDGE_CURVE('',#696,#769,#639,.T.);
#939=EDGE_CURVE('',#768,#770,#640,.T.);
#940=EDGE_CURVE('',#771,#695,#461,.T.);
#941=EDGE_CURVE('',#770,#771,#462,.T.);
#942=EDGE_CURVE('',#772,#773,#463,.T.);
#943=EDGE_CURVE('',#773,#695,#641,.T.);
#944=EDGE_CURVE('',#771,#772,#642,.T.);
#945=EDGE_CURVE('',#772,#774,#643,.T.);
#946=EDGE_CURVE('',#774,#775,#464,.T.);
#947=EDGE_CURVE('',#775,#773,#644,.T.);
#948=EDGE_CURVE('',#719,#775,#645,.T.);
#949=EDGE_CURVE('',#774,#753,#646,.T.);
#950=EDGE_CURVE('',#767,#776,#465,.T.);
#951=EDGE_CURVE('',#712,#776,#647,.T.);
#952=EDGE_CURVE('',#777,#769,#466,.T.);
#953=EDGE_CURVE('',#776,#777,#648,.T.);
#954=EDGE_CURVE('',#777,#698,#649,.T.);
#955=EDGE_CURVE('',#773,#778,#467,.T.);
#956=EDGE_CURVE('',#697,#778,#650,.T.);
#957=EDGE_CURVE('',#779,#775,#468,.T.);
#958=EDGE_CURVE('',#778,#779,#651,.T.);
#959=EDGE_CURVE('',#779,#721,#652,.T.);
#960=EDGE_CURVE('',#780,#780,#653,.T.);
#961=EDGE_CURVE('',#781,#781,#654,.T.);
#962=EDGE_CURVE('',#781,#780,#469,.T.);
#963=EDGE_CURVE('',#782,#782,#655,.T.);
#964=EDGE_CURVE('',#782,#781,#470,.T.);
#965=EDGE_CURVE('',#783,#783,#656,.T.);
#966=EDGE_CURVE('',#783,#782,#471,.T.);
#967=EDGE_CURVE('',#784,#785,#657,.T.);
#968=EDGE_CURVE('',#786,#784,#658,.T.);
#969=EDGE_CURVE('',#787,#786,#659,.T.);
#970=EDGE_CURVE('',#788,#787,#472,.T.);
#971=EDGE_CURVE('',#789,#788,#660,.T.);
#972=EDGE_CURVE('',#790,#789,#661,.T.);
#973=EDGE_CURVE('',#791,#790,#662,.T.);
#974=EDGE_CURVE('',#792,#791,#473,.T.);
#975=EDGE_CURVE('',#793,#792,#663,.T.);
#976=EDGE_CURVE('',#794,#793,#664,.T.);
#977=EDGE_CURVE('',#795,#794,#665,.T.);
#978=EDGE_CURVE('',#796,#795,#474,.T.);
#979=EDGE_CURVE('',#797,#796,#666,.T.);
#980=EDGE_CURVE('',#798,#797,#667,.T.);
#981=EDGE_CURVE('',#799,#798,#668,.T.);
#982=EDGE_CURVE('',#785,#799,#475,.T.);
#983=EDGE_CURVE('',#785,#712,#476,.T.);
#984=EDGE_CURVE('',#776,#784,#477,.T.);
#985=EDGE_CURVE('',#799,#713,#478,.T.);
#986=EDGE_CURVE('',#798,#800,#479,.T.);
#987=EDGE_CURVE('',#800,#713,#669,.T.);
#988=EDGE_CURVE('',#797,#801,#480,.T.);
#989=EDGE_CURVE('',#801,#800,#670,.T.);
#990=EDGE_CURVE('',#796,#688,#481,.T.);
#991=EDGE_CURVE('',#688,#801,#671,.T.);
#992=EDGE_CURVE('',#795,#689,#482,.T.);
#993=EDGE_CURVE('',#794,#802,#483,.T.);
#994=EDGE_CURVE('',#802,#689,#672,.T.);
#995=EDGE_CURVE('',#793,#803,#484,.T.);
#996=EDGE_CURVE('',#803,#802,#673,.T.);
#997=EDGE_CURVE('',#792,#720,#485,.T.);
#998=EDGE_CURVE('',#720,#803,#674,.T.);
#999=EDGE_CURVE('',#791,#721,#486,.T.);
#1000=EDGE_CURVE('',#790,#779,#487,.T.);
#1001=EDGE_CURVE('',#789,#778,#488,.T.);
#1002=EDGE_CURVE('',#788,#697,#489,.T.);
#1003=EDGE_CURVE('',#787,#698,#490,.T.);
#1004=EDGE_CURVE('',#786,#777,#491,.T.);
#1005=EDGE_CURVE('',#755,#803,#492,.T.);
#1006=EDGE_CURVE('',#802,#757,#493,.T.);
#1007=EDGE_CURVE('',#761,#801,#494,.T.);
#1008=EDGE_CURVE('',#800,#763,#495,.T.);
#1024=ORIENTED_EDGE('',*,*,#814,.T.);
#1025=ORIENTED_EDGE('',*,*,#815,.T.);
#1026=ORIENTED_EDGE('',*,*,#816,.T.);
#1027=ORIENTED_EDGE('',*,*,#815,.F.);
#1028=ORIENTED_EDGE('',*,*,#817,.F.);
#1029=ORIENTED_EDGE('',*,*,#818,.F.);
#1030=ORIENTED_EDGE('',*,*,#819,.F.);
#1031=ORIENTED_EDGE('',*,*,#820,.F.);
#1032=ORIENTED_EDGE('',*,*,#821,.F.);
#1033=ORIENTED_EDGE('',*,*,#814,.F.);
#1034=ORIENTED_EDGE('',*,*,#822,.F.);
#1035=ORIENTED_EDGE('',*,*,#823,.F.);
#1036=ORIENTED_EDGE('',*,*,#824,.T.);
#1037=ORIENTED_EDGE('',*,*,#816,.F.);
#1038=ORIENTED_EDGE('',*,*,#824,.F.);
#1039=ORIENTED_EDGE('',*,*,#825,.T.);
#1040=ORIENTED_EDGE('',*,*,#826,.T.);
#1041=ORIENTED_EDGE('',*,*,#827,.T.);
#1042=ORIENTED_EDGE('',*,*,#826,.F.);
#1043=ORIENTED_EDGE('',*,*,#828,.F.);
#1044=ORIENTED_EDGE('',*,*,#829,.F.);
#1045=ORIENTED_EDGE('',*,*,#830,.F.);
#1046=ORIENTED_EDGE('',*,*,#831,.F.);
#1047=ORIENTED_EDGE('',*,*,#832,.F.);
#1048=ORIENTED_EDGE('',*,*,#825,.F.);
#1049=ORIENTED_EDGE('',*,*,#827,.F.);
#1050=ORIENTED_EDGE('',*,*,#833,.T.);
#1051=ORIENTED_EDGE('',*,*,#834,.F.);
#1052=ORIENTED_EDGE('',*,*,#835,.F.);
#1053=ORIENTED_EDGE('',*,*,#833,.F.);
#1054=ORIENTED_EDGE('',*,*,#821,.T.);
#1055=ORIENTED_EDGE('',*,*,#836,.T.);
#1056=ORIENTED_EDGE('',*,*,#837,.T.);
#1057=ORIENTED_EDGE('',*,*,#836,.F.);
#1058=ORIENTED_EDGE('',*,*,#838,.F.);
#1059=ORIENTED_EDGE('',*,*,#839,.F.);
#1060=ORIENTED_EDGE('',*,*,#840,.T.);
#1061=ORIENTED_EDGE('',*,*,#837,.F.);
#1062=ORIENTED_EDGE('',*,*,#840,.F.);
#1063=ORIENTED_EDGE('',*,*,#832,.T.);
#1064=ORIENTED_EDGE('',*,*,#841,.T.);
#1065=ORIENTED_EDGE('',*,*,#842,.T.);
#1066=ORIENTED_EDGE('',*,*,#841,.F.);
#1067=ORIENTED_EDGE('',*,*,#842,.F.);
#1068=ORIENTED_EDGE('',*,*,#843,.T.);
#1069=ORIENTED_EDGE('',*,*,#844,.F.);
#1070=ORIENTED_EDGE('',*,*,#845,.F.);
#1071=ORIENTED_EDGE('',*,*,#843,.F.);
#1072=ORIENTED_EDGE('',*,*,#846,.T.);
#1073=ORIENTED_EDGE('',*,*,#847,.T.);
#1074=ORIENTED_EDGE('',*,*,#848,.T.);
#1075=ORIENTED_EDGE('',*,*,#847,.F.);
#1076=ORIENTED_EDGE('',*,*,#849,.F.);
#1077=ORIENTED_EDGE('',*,*,#850,.F.);
#1078=ORIENTED_EDGE('',*,*,#851,.F.);
#1079=ORIENTED_EDGE('',*,*,#852,.F.);
#1080=ORIENTED_EDGE('',*,*,#853,.F.);
#1081=ORIENTED_EDGE('',*,*,#846,.F.);
#1082=ORIENTED_EDGE('',*,*,#854,.F.);
#1083=ORIENTED_EDGE('',*,*,#855,.T.);
#1084=ORIENTED_EDGE('',*,*,#848,.F.);
#1085=ORIENTED_EDGE('',*,*,#855,.F.);
#1086=ORIENTED_EDGE('',*,*,#856,.T.);
#1087=ORIENTED_EDGE('',*,*,#857,.T.);
#1088=ORIENTED_EDGE('',*,*,#858,.T.);
#1089=ORIENTED_EDGE('',*,*,#857,.F.);
#1090=ORIENTED_EDGE('',*,*,#859,.F.);
#1091=ORIENTED_EDGE('',*,*,#860,.F.);
#1092=ORIENTED_EDGE('',*,*,#861,.F.);
#1093=ORIENTED_EDGE('',*,*,#862,.F.);
#1094=ORIENTED_EDGE('',*,*,#863,.F.);
#1095=ORIENTED_EDGE('',*,*,#856,.F.);
#1096=ORIENTED_EDGE('',*,*,#858,.F.);
#1097=ORIENTED_EDGE('',*,*,#864,.T.);
#1098=ORIENTED_EDGE('',*,*,#865,.F.);
#1099=ORIENTED_EDGE('',*,*,#864,.F.);
#1100=ORIENTED_EDGE('',*,*,#853,.T.);
#1101=ORIENTED_EDGE('',*,*,#866,.T.);
#1102=ORIENTED_EDGE('',*,*,#867,.T.);
#1103=ORIENTED_EDGE('',*,*,#866,.F.);
#1104=ORIENTED_EDGE('',*,*,#868,.F.);
#1105=ORIENTED_EDGE('',*,*,#869,.T.);
#1106=ORIENTED_EDGE('',*,*,#867,.F.);
#1107=ORIENTED_EDGE('',*,*,#869,.F.);
#1108=ORIENTED_EDGE('',*,*,#863,.T.);
#1109=ORIENTED_EDGE('',*,*,#870,.T.);
#1110=ORIENTED_EDGE('',*,*,#871,.T.);
#1111=ORIENTED_EDGE('',*,*,#870,.F.);
#1112=ORIENTED_EDGE('',*,*,#871,.F.);
#1113=ORIENTED_EDGE('',*,*,#872,.T.);
#1114=ORIENTED_EDGE('',*,*,#873,.F.);
#1115=ORIENTED_EDGE('',*,*,#872,.F.);
#1116=ORIENTED_EDGE('',*,*,#874,.F.);
#1117=ORIENTED_EDGE('',*,*,#875,.F.);
#1118=ORIENTED_EDGE('',*,*,#876,.T.);
#1119=ORIENTED_EDGE('',*,*,#877,.F.);
#1120=ORIENTED_EDGE('',*,*,#878,.F.);
#1121=ORIENTED_EDGE('',*,*,#876,.F.);
#1122=ORIENTED_EDGE('',*,*,#879,.F.);
#1123=ORIENTED_EDGE('',*,*,#880,.F.);
#1124=ORIENTED_EDGE('',*,*,#881,.T.);
#1125=ORIENTED_EDGE('',*,*,#882,.F.);
#1126=ORIENTED_EDGE('',*,*,#883,.F.);
#1127=ORIENTED_EDGE('',*,*,#881,.F.);
#1128=ORIENTED_EDGE('',*,*,#884,.F.);
#1129=ORIENTED_EDGE('',*,*,#885,.F.);
#1130=ORIENTED_EDGE('',*,*,#886,.T.);
#1131=ORIENTED_EDGE('',*,*,#887,.F.);
#1132=ORIENTED_EDGE('',*,*,#888,.F.);
#1133=ORIENTED_EDGE('',*,*,#886,.F.);
#1134=ORIENTED_EDGE('',*,*,#889,.F.);
#1135=ORIENTED_EDGE('',*,*,#890,.F.);
#1136=ORIENTED_EDGE('',*,*,#891,.T.);
#1137=ORIENTED_EDGE('',*,*,#892,.F.);
#1138=ORIENTED_EDGE('',*,*,#893,.F.);
#1139=ORIENTED_EDGE('',*,*,#891,.F.);
#1140=ORIENTED_EDGE('',*,*,#894,.F.);
#1141=ORIENTED_EDGE('',*,*,#895,.T.);
#1142=ORIENTED_EDGE('',*,*,#896,.F.);
#1143=ORIENTED_EDGE('',*,*,#895,.F.);
#1144=ORIENTED_EDGE('',*,*,#838,.T.);
#1145=ORIENTED_EDGE('',*,*,#839,.T.);
#1146=ORIENTED_EDGE('',*,*,#882,.T.);
#1147=ORIENTED_EDGE('',*,*,#883,.T.);
#1148=ORIENTED_EDGE('',*,*,#822,.T.);
#1149=ORIENTED_EDGE('',*,*,#823,.T.);
#1150=ORIENTED_EDGE('',*,*,#892,.T.);
#1151=ORIENTED_EDGE('',*,*,#893,.T.);
#1152=ORIENTED_EDGE('',*,*,#894,.T.);
#1153=ORIENTED_EDGE('',*,*,#897,.F.);
#1154=ORIENTED_EDGE('',*,*,#898,.T.);
#1155=ORIENTED_EDGE('',*,*,#899,.F.);
#1156=ORIENTED_EDGE('',*,*,#898,.F.);
#1157=ORIENTED_EDGE('',*,*,#874,.T.);
#1158=ORIENTED_EDGE('',*,*,#875,.T.);
#1159=ORIENTED_EDGE('',*,*,#844,.T.);
#1160=ORIENTED_EDGE('',*,*,#845,.T.);
#1161=ORIENTED_EDGE('',*,*,#884,.T.);
#1162=ORIENTED_EDGE('',*,*,#885,.T.);
#1163=ORIENTED_EDGE('',*,*,#834,.T.);
#1164=ORIENTED_EDGE('',*,*,#835,.T.);
#1165=ORIENTED_EDGE('',*,*,#897,.T.);
#1166=ORIENTED_EDGE('',*,*,#900,.F.);
#1167=ORIENTED_EDGE('',*,*,#901,.T.);
#1168=ORIENTED_EDGE('',*,*,#902,.F.);
#1169=ORIENTED_EDGE('',*,*,#901,.F.);
#1170=ORIENTED_EDGE('',*,*,#900,.T.);
#1171=ORIENTED_EDGE('',*,*,#903,.F.);
#1172=ORIENTED_EDGE('',*,*,#904,.T.);
#1173=ORIENTED_EDGE('',*,*,#905,.F.);
#1174=ORIENTED_EDGE('',*,*,#904,.F.);
#1175=ORIENTED_EDGE('',*,*,#903,.T.);
#1176=ORIENTED_EDGE('',*,*,#906,.T.);
#1177=ORIENTED_EDGE('',*,*,#859,.T.);
#1178=ORIENTED_EDGE('',*,*,#907,.T.);
#1179=ORIENTED_EDGE('',*,*,#908,.T.);
#1180=ORIENTED_EDGE('',*,*,#909,.T.);
#1181=ORIENTED_EDGE('',*,*,#910,.T.);
#1182=ORIENTED_EDGE('',*,*,#906,.F.);
#1183=ORIENTED_EDGE('',*,*,#911,.T.);
#1184=ORIENTED_EDGE('',*,*,#909,.F.);
#1185=ORIENTED_EDGE('',*,*,#912,.T.);
#1186=ORIENTED_EDGE('',*,*,#913,.T.);
#1187=ORIENTED_EDGE('',*,*,#914,.T.);
#1188=ORIENTED_EDGE('',*,*,#915,.T.);
#1189=ORIENTED_EDGE('',*,*,#916,.T.);
#1190=ORIENTED_EDGE('',*,*,#913,.F.);
#1191=ORIENTED_EDGE('',*,*,#917,.T.);
#1192=ORIENTED_EDGE('',*,*,#918,.T.);
#1193=ORIENTED_EDGE('',*,*,#817,.T.);
#1194=ORIENTED_EDGE('',*,*,#915,.F.);
#1195=ORIENTED_EDGE('',*,*,#919,.T.);
#1196=ORIENTED_EDGE('',*,*,#920,.T.);
#1197=ORIENTED_EDGE('',*,*,#921,.T.);
#1198=ORIENTED_EDGE('',*,*,#918,.F.);
#1199=ORIENTED_EDGE('',*,*,#922,.T.);
#1200=ORIENTED_EDGE('',*,*,#920,.F.);
#1201=ORIENTED_EDGE('',*,*,#923,.T.);
#1202=ORIENTED_EDGE('',*,*,#924,.T.);
#1203=ORIENTED_EDGE('',*,*,#925,.T.);
#1204=ORIENTED_EDGE('',*,*,#926,.T.);
#1205=ORIENTED_EDGE('',*,*,#927,.T.);
#1206=ORIENTED_EDGE('',*,*,#924,.F.);
#1207=ORIENTED_EDGE('',*,*,#928,.T.);
#1208=ORIENTED_EDGE('',*,*,#929,.T.);
#1209=ORIENTED_EDGE('',*,*,#849,.T.);
#1210=ORIENTED_EDGE('',*,*,#926,.F.);
#1211=ORIENTED_EDGE('',*,*,#930,.T.);
#1212=ORIENTED_EDGE('',*,*,#931,.T.);
#1213=ORIENTED_EDGE('',*,*,#932,.T.);
#1214=ORIENTED_EDGE('',*,*,#929,.F.);
#1215=ORIENTED_EDGE('',*,*,#933,.T.);
#1216=ORIENTED_EDGE('',*,*,#931,.F.);
#1217=ORIENTED_EDGE('',*,*,#934,.T.);
#1218=ORIENTED_EDGE('',*,*,#935,.T.);
#1219=ORIENTED_EDGE('',*,*,#936,.T.);
#1220=ORIENTED_EDGE('',*,*,#937,.T.);
#1221=ORIENTED_EDGE('',*,*,#938,.T.);
#1222=ORIENTED_EDGE('',*,*,#935,.F.);
#1223=ORIENTED_EDGE('',*,*,#939,.T.);
#1224=ORIENTED_EDGE('',*,*,#940,.T.);
#1225=ORIENTED_EDGE('',*,*,#828,.T.);
#1226=ORIENTED_EDGE('',*,*,#937,.F.);
#1227=ORIENTED_EDGE('',*,*,#941,.T.);
#1228=ORIENTED_EDGE('',*,*,#942,.T.);
#1229=ORIENTED_EDGE('',*,*,#943,.T.);
#1230=ORIENTED_EDGE('',*,*,#940,.F.);
#1231=ORIENTED_EDGE('',*,*,#944,.T.);
#1232=ORIENTED_EDGE('',*,*,#942,.F.);
#1233=ORIENTED_EDGE('',*,*,#945,.T.);
#1234=ORIENTED_EDGE('',*,*,#946,.T.);
#1235=ORIENTED_EDGE('',*,*,#947,.T.);
#1236=ORIENTED_EDGE('',*,*,#907,.F.);
#1237=ORIENTED_EDGE('',*,*,#948,.T.);
#1238=ORIENTED_EDGE('',*,*,#946,.F.);
#1239=ORIENTED_EDGE('',*,*,#949,.T.);
#1240=ORIENTED_EDGE('',*,*,#932,.F.);
#1241=ORIENTED_EDGE('',*,*,#950,.T.);
#1242=ORIENTED_EDGE('',*,*,#951,.F.);
#1243=ORIENTED_EDGE('',*,*,#850,.T.);
#1244=ORIENTED_EDGE('',*,*,#936,.F.);
#1245=ORIENTED_EDGE('',*,*,#952,.F.);
#1246=ORIENTED_EDGE('',*,*,#953,.F.);
#1247=ORIENTED_EDGE('',*,*,#950,.F.);
#1248=ORIENTED_EDGE('',*,*,#938,.F.);
#1249=ORIENTED_EDGE('',*,*,#831,.T.);
#1250=ORIENTED_EDGE('',*,*,#954,.F.);
#1251=ORIENTED_EDGE('',*,*,#952,.T.);
#1252=ORIENTED_EDGE('',*,*,#943,.F.);
#1253=ORIENTED_EDGE('',*,*,#955,.T.);
#1254=ORIENTED_EDGE('',*,*,#956,.F.);
#1255=ORIENTED_EDGE('',*,*,#829,.T.);
#1256=ORIENTED_EDGE('',*,*,#947,.F.);
#1257=ORIENTED_EDGE('',*,*,#957,.F.);
#1258=ORIENTED_EDGE('',*,*,#958,.F.);
#1259=ORIENTED_EDGE('',*,*,#955,.F.);
#1260=ORIENTED_EDGE('',*,*,#948,.F.);
#1261=ORIENTED_EDGE('',*,*,#862,.T.);
#1262=ORIENTED_EDGE('',*,*,#959,.F.);
#1263=ORIENTED_EDGE('',*,*,#957,.T.);
#1264=ORIENTED_EDGE('',*,*,#908,.F.);
#1265=ORIENTED_EDGE('',*,*,#949,.F.);
#1266=ORIENTED_EDGE('',*,*,#945,.F.);
#1267=ORIENTED_EDGE('',*,*,#944,.F.);
#1268=ORIENTED_EDGE('',*,*,#941,.F.);
#1269=ORIENTED_EDGE('',*,*,#939,.F.);
#1270=ORIENTED_EDGE('',*,*,#934,.F.);
#1271=ORIENTED_EDGE('',*,*,#933,.F.);
#1272=ORIENTED_EDGE('',*,*,#930,.F.);
#1273=ORIENTED_EDGE('',*,*,#928,.F.);
#1274=ORIENTED_EDGE('',*,*,#923,.F.);
#1275=ORIENTED_EDGE('',*,*,#922,.F.);
#1276=ORIENTED_EDGE('',*,*,#919,.F.);
#1277=ORIENTED_EDGE('',*,*,#917,.F.);
#1278=ORIENTED_EDGE('',*,*,#912,.F.);
#1279=ORIENTED_EDGE('',*,*,#911,.F.);
#1280=ORIENTED_EDGE('',*,*,#960,.F.);
#1281=ORIENTED_EDGE('',*,*,#961,.T.);
#1282=ORIENTED_EDGE('',*,*,#962,.T.);
#1283=ORIENTED_EDGE('',*,*,#960,.T.);
#1284=ORIENTED_EDGE('',*,*,#962,.F.);
#1285=ORIENTED_EDGE('',*,*,#963,.F.);
#1286=ORIENTED_EDGE('',*,*,#964,.T.);
#1287=ORIENTED_EDGE('',*,*,#961,.F.);
#1288=ORIENTED_EDGE('',*,*,#964,.F.);
#1289=ORIENTED_EDGE('',*,*,#868,.T.);
#1290=ORIENTED_EDGE('',*,*,#873,.T.);
#1291=ORIENTED_EDGE('',*,*,#854,.T.);
#1292=ORIENTED_EDGE('',*,*,#865,.T.);
#1293=ORIENTED_EDGE('',*,*,#879,.T.);
#1294=ORIENTED_EDGE('',*,*,#880,.T.);
#1295=ORIENTED_EDGE('',*,*,#877,.T.);
#1296=ORIENTED_EDGE('',*,*,#878,.T.);
#1297=ORIENTED_EDGE('',*,*,#889,.T.);
#1298=ORIENTED_EDGE('',*,*,#890,.T.);
#1299=ORIENTED_EDGE('',*,*,#887,.T.);
#1300=ORIENTED_EDGE('',*,*,#888,.T.);
#1301=ORIENTED_EDGE('',*,*,#965,.T.);
#1302=ORIENTED_EDGE('',*,*,#966,.T.);
#1303=ORIENTED_EDGE('',*,*,#963,.T.);
#1304=ORIENTED_EDGE('',*,*,#966,.F.);
#1305=ORIENTED_EDGE('',*,*,#967,.F.);
#1306=ORIENTED_EDGE('',*,*,#968,.F.);
#1307=ORIENTED_EDGE('',*,*,#969,.F.);
#1308=ORIENTED_EDGE('',*,*,#970,.F.);
#1309=ORIENTED_EDGE('',*,*,#971,.F.);
#1310=ORIENTED_EDGE('',*,*,#972,.F.);
#1311=ORIENTED_EDGE('',*,*,#973,.F.);
#1312=ORIENTED_EDGE('',*,*,#974,.F.);
#1313=ORIENTED_EDGE('',*,*,#975,.F.);
#1314=ORIENTED_EDGE('',*,*,#976,.F.);
#1315=ORIENTED_EDGE('',*,*,#977,.F.);
#1316=ORIENTED_EDGE('',*,*,#978,.F.);
#1317=ORIENTED_EDGE('',*,*,#979,.F.);
#1318=ORIENTED_EDGE('',*,*,#980,.F.);
#1319=ORIENTED_EDGE('',*,*,#981,.F.);
#1320=ORIENTED_EDGE('',*,*,#982,.F.);
#1321=ORIENTED_EDGE('',*,*,#896,.T.);
#1322=ORIENTED_EDGE('',*,*,#899,.T.);
#1323=ORIENTED_EDGE('',*,*,#902,.T.);
#1324=ORIENTED_EDGE('',*,*,#905,.T.);
#1325=ORIENTED_EDGE('',*,*,#965,.F.);
#1326=ORIENTED_EDGE('',*,*,#983,.T.);
#1327=ORIENTED_EDGE('',*,*,#951,.T.);
#1328=ORIENTED_EDGE('',*,*,#984,.T.);
#1329=ORIENTED_EDGE('',*,*,#967,.T.);
#1330=ORIENTED_EDGE('',*,*,#983,.F.);
#1331=ORIENTED_EDGE('',*,*,#982,.T.);
#1332=ORIENTED_EDGE('',*,*,#985,.T.);
#1333=ORIENTED_EDGE('',*,*,#851,.T.);
#1334=ORIENTED_EDGE('',*,*,#986,.T.);
#1335=ORIENTED_EDGE('',*,*,#987,.T.);
#1336=ORIENTED_EDGE('',*,*,#985,.F.);
#1337=ORIENTED_EDGE('',*,*,#981,.T.);
#1338=ORIENTED_EDGE('',*,*,#986,.F.);
#1339=ORIENTED_EDGE('',*,*,#980,.T.);
#1340=ORIENTED_EDGE('',*,*,#988,.T.);
#1341=ORIENTED_EDGE('',*,*,#989,.T.);
#1342=ORIENTED_EDGE('',*,*,#990,.T.);
#1343=ORIENTED_EDGE('',*,*,#991,.T.);
#1344=ORIENTED_EDGE('',*,*,#988,.F.);
#1345=ORIENTED_EDGE('',*,*,#979,.T.);
#1346=ORIENTED_EDGE('',*,*,#990,.F.);
#1347=ORIENTED_EDGE('',*,*,#978,.T.);
#1348=ORIENTED_EDGE('',*,*,#992,.T.);
#1349=ORIENTED_EDGE('',*,*,#819,.T.);
#1350=ORIENTED_EDGE('',*,*,#993,.T.);
#1351=ORIENTED_EDGE('',*,*,#994,.T.);
#1352=ORIENTED_EDGE('',*,*,#992,.F.);
#1353=ORIENTED_EDGE('',*,*,#977,.T.);
#1354=ORIENTED_EDGE('',*,*,#993,.F.);
#1355=ORIENTED_EDGE('',*,*,#976,.T.);
#1356=ORIENTED_EDGE('',*,*,#995,.T.);
#1357=ORIENTED_EDGE('',*,*,#996,.T.);
#1358=ORIENTED_EDGE('',*,*,#997,.T.);
#1359=ORIENTED_EDGE('',*,*,#998,.T.);
#1360=ORIENTED_EDGE('',*,*,#995,.F.);
#1361=ORIENTED_EDGE('',*,*,#975,.T.);
#1362=ORIENTED_EDGE('',*,*,#997,.F.);
#1363=ORIENTED_EDGE('',*,*,#974,.T.);
#1364=ORIENTED_EDGE('',*,*,#999,.T.);
#1365=ORIENTED_EDGE('',*,*,#861,.T.);
#1366=ORIENTED_EDGE('',*,*,#1000,.T.);
#1367=ORIENTED_EDGE('',*,*,#959,.T.);
#1368=ORIENTED_EDGE('',*,*,#999,.F.);
#1369=ORIENTED_EDGE('',*,*,#973,.T.);
#1370=ORIENTED_EDGE('',*,*,#1000,.F.);
#1371=ORIENTED_EDGE('',*,*,#972,.T.);
#1372=ORIENTED_EDGE('',*,*,#1001,.T.);
#1373=ORIENTED_EDGE('',*,*,#958,.T.);
#1374=ORIENTED_EDGE('',*,*,#1002,.T.);
#1375=ORIENTED_EDGE('',*,*,#956,.T.);
#1376=ORIENTED_EDGE('',*,*,#1001,.F.);
#1377=ORIENTED_EDGE('',*,*,#971,.T.);
#1378=ORIENTED_EDGE('',*,*,#1002,.F.);
#1379=ORIENTED_EDGE('',*,*,#970,.T.);
#1380=ORIENTED_EDGE('',*,*,#1003,.T.);
#1381=ORIENTED_EDGE('',*,*,#830,.T.);
#1382=ORIENTED_EDGE('',*,*,#1004,.T.);
#1383=ORIENTED_EDGE('',*,*,#954,.T.);
#1384=ORIENTED_EDGE('',*,*,#1003,.F.);
#1385=ORIENTED_EDGE('',*,*,#969,.T.);
#1386=ORIENTED_EDGE('',*,*,#1004,.F.);
#1387=ORIENTED_EDGE('',*,*,#968,.T.);
#1388=ORIENTED_EDGE('',*,*,#984,.F.);
#1389=ORIENTED_EDGE('',*,*,#953,.T.);
#1390=ORIENTED_EDGE('',*,*,#910,.F.);
#1391=ORIENTED_EDGE('',*,*,#1005,.T.);
#1392=ORIENTED_EDGE('',*,*,#998,.F.);
#1393=ORIENTED_EDGE('',*,*,#860,.T.);
#1394=ORIENTED_EDGE('',*,*,#916,.F.);
#1395=ORIENTED_EDGE('',*,*,#820,.T.);
#1396=ORIENTED_EDGE('',*,*,#994,.F.);
#1397=ORIENTED_EDGE('',*,*,#1006,.T.);
#1398=ORIENTED_EDGE('',*,*,#921,.F.);
#1399=ORIENTED_EDGE('',*,*,#1007,.T.);
#1400=ORIENTED_EDGE('',*,*,#991,.F.);
#1401=ORIENTED_EDGE('',*,*,#818,.T.);
#1402=ORIENTED_EDGE('',*,*,#927,.F.);
#1403=ORIENTED_EDGE('',*,*,#852,.T.);
#1404=ORIENTED_EDGE('',*,*,#987,.F.);
#1405=ORIENTED_EDGE('',*,*,#1008,.T.);
#1406=ORIENTED_EDGE('',*,*,#925,.F.);
#1407=ORIENTED_EDGE('',*,*,#1008,.F.);
#1408=ORIENTED_EDGE('',*,*,#989,.F.);
#1409=ORIENTED_EDGE('',*,*,#1007,.F.);
#1410=ORIENTED_EDGE('',*,*,#914,.F.);
#1411=ORIENTED_EDGE('',*,*,#1006,.F.);
#1412=ORIENTED_EDGE('',*,*,#996,.F.);
#1413=ORIENTED_EDGE('',*,*,#1005,.F.);
#1444=CONICAL_SURFACE('',#1625,1.35,0.785398163397448);
#1445=CONICAL_SURFACE('',#1631,1.35,0.785398163397448);
#1446=CONICAL_SURFACE('',#1637,1.35,0.785398163397448);
#1447=CONICAL_SURFACE('',#1640,1.35,0.785398163397448);
#1448=CONICAL_SURFACE('',#1643,1.35,0.785398163397448);
#1449=CONICAL_SURFACE('',#1649,1.35,0.785398163397448);
#1450=CONICAL_SURFACE('',#1655,1.35,0.785398163397448);
#1451=CONICAL_SURFACE('',#1658,1.35,0.785398163397448);
#1452=CONICAL_SURFACE('',#1682,1.8,0.78539816339745);
#1453=CONICAL_SURFACE('',#1685,21.6,0.785398163397445);
#1454=CONICAL_SURFACE('',#1688,1.8,0.78539816339745);
#1455=CONICAL_SURFACE('',#1692,1.8,0.78539816339745);
#1456=CONICAL_SURFACE('',#1695,21.6,0.785398163397451);
#1457=CONICAL_SURFACE('',#1698,1.8,0.78539816339745);
#1458=CONICAL_SURFACE('',#1702,1.8,0.78539816339745);
#1459=CONICAL_SURFACE('',#1705,21.6,0.785398163397451);
#1460=CONICAL_SURFACE('',#1708,1.8,0.78539816339745);
#1461=CONICAL_SURFACE('',#1712,1.8,0.78539816339745);
#1462=CONICAL_SURFACE('',#1715,21.6,0.785398163397451);
#1463=CONICAL_SURFACE('',#1718,1.8,0.78539816339745);
#1464=CONICAL_SURFACE('',#1735,13.7,0.785398163397449);
#1465=CONICAL_SURFACE('',#1739,13.9,0.785398163397449);
#1466=CONICAL_SURFACE('',#1754,1.6,0.785398163397447);
#1467=CONICAL_SURFACE('',#1756,1.6,0.785398163397447);
#1468=CONICAL_SURFACE('',#1758,21.8,0.785398163397448);
#1469=CONICAL_SURFACE('',#1760,1.6,0.785398163397447);
#1470=CONICAL_SURFACE('',#1763,1.6,0.785398163397447);
#1471=CONICAL_SURFACE('',#1765,21.8,0.785398163397446);
#1472=CONICAL_SURFACE('',#1767,1.6,0.785398163397447);
#1473=CONICAL_SURFACE('',#1770,1.6,0.785398163397447);
#1474=CONICAL_SURFACE('',#1771,21.8,0.785398163397448);
#1475=CONICAL_SURFACE('',#1772,1.6,0.785398163397447);
#1476=CONICAL_SURFACE('',#1774,1.6,0.785398163397447);
#1477=CONICAL_SURFACE('',#1775,21.8,0.785398163397449);
#1482=ADVANCED_FACE('',(#191),#1444,.F.);
#1483=ADVANCED_FACE('',(#192,#139,#140),#169,.T.);
#1484=ADVANCED_FACE('',(#193),#108,.F.);
#1485=ADVANCED_FACE('',(#194),#1445,.F.);
#1486=ADVANCED_FACE('',(#195,#141,#142),#170,.T.);
#1487=ADVANCED_FACE('',(#196),#109,.F.);
#1488=ADVANCED_FACE('',(#197),#1446,.F.);
#1489=ADVANCED_FACE('',(#198),#110,.F.);
#1490=ADVANCED_FACE('',(#199),#1447,.F.);
#1491=ADVANCED_FACE('',(#200),#111,.F.);
#1492=ADVANCED_FACE('',(#201),#1448,.F.);
#1493=ADVANCED_FACE('',(#202,#143,#144),#171,.T.);
#1494=ADVANCED_FACE('',(#203),#112,.F.);
#1495=ADVANCED_FACE('',(#204),#1449,.F.);
#1496=ADVANCED_FACE('',(#205,#145,#146),#172,.T.);
#1497=ADVANCED_FACE('',(#206),#113,.F.);
#1498=ADVANCED_FACE('',(#207),#1450,.F.);
#1499=ADVANCED_FACE('',(#208),#114,.F.);
#1500=ADVANCED_FACE('',(#209),#1451,.F.);
#1501=ADVANCED_FACE('',(#210),#115,.F.);
#1502=ADVANCED_FACE('',(#211),#116,.F.);
#1503=ADVANCED_FACE('',(#212),#117,.F.);
#1504=ADVANCED_FACE('',(#213),#118,.F.);
#1505=ADVANCED_FACE('',(#214),#119,.F.);
#1506=ADVANCED_FACE('',(#215,#147,#148,#149,#150),#120,.F.);
#1507=ADVANCED_FACE('',(#216),#173,.T.);
#1508=ADVANCED_FACE('',(#217,#151,#152,#153,#154),#121,.F.);
#1509=ADVANCED_FACE('',(#218),#174,.T.);
#1510=ADVANCED_FACE('',(#219),#122,.F.);
#1511=ADVANCED_FACE('',(#220),#175,.T.);
#1512=ADVANCED_FACE('',(#221),#123,.F.);
#1513=ADVANCED_FACE('',(#222),#176,.T.);
#1514=ADVANCED_FACE('',(#223),#177,.T.);
#1515=ADVANCED_FACE('',(#224),#1452,.T.);
#1516=ADVANCED_FACE('',(#225),#1453,.F.);
#1517=ADVANCED_FACE('',(#226),#1454,.T.);
#1518=ADVANCED_FACE('',(#227),#178,.T.);
#1519=ADVANCED_FACE('',(#228),#1455,.T.);
#1520=ADVANCED_FACE('',(#229),#1456,.F.);
#1521=ADVANCED_FACE('',(#230),#1457,.T.);
#1522=ADVANCED_FACE('',(#231),#179,.T.);
#1523=ADVANCED_FACE('',(#232),#1458,.T.);
#1524=ADVANCED_FACE('',(#233),#1459,.F.);
#1525=ADVANCED_FACE('',(#234),#1460,.T.);
#1526=ADVANCED_FACE('',(#235),#180,.T.);
#1527=ADVANCED_FACE('',(#236),#1461,.T.);
#1528=ADVANCED_FACE('',(#237),#1462,.F.);
#1529=ADVANCED_FACE('',(#238),#1463,.T.);
#1530=ADVANCED_FACE('',(#239),#124,.T.);
#1531=ADVANCED_FACE('',(#240),#125,.F.);
#1532=ADVANCED_FACE('',(#241),#126,.T.);
#1533=ADVANCED_FACE('',(#242),#127,.T.);
#1534=ADVANCED_FACE('',(#243),#128,.F.);
#1535=ADVANCED_FACE('',(#244),#129,.T.);
#1536=ADVANCED_FACE('',(#245,#155),#181,.F.);
#1537=ADVANCED_FACE('',(#246),#1464,.F.);
#1538=ADVANCED_FACE('',(#247,#156,#157,#158,#159,#160,#161,#162,#163),#130,
 .F.);
#1539=ADVANCED_FACE('',(#248),#1465,.F.);
#1540=ADVANCED_FACE('',(#249,#164,#165,#166,#167,#168),#182,.T.);
#1541=ADVANCED_FACE('',(#250),#1466,.T.);
#1542=ADVANCED_FACE('',(#251),#183,.T.);
#1543=ADVANCED_FACE('',(#252),#1467,.T.);
#1544=ADVANCED_FACE('',(#253),#1468,.F.);
#1545=ADVANCED_FACE('',(#254),#1469,.T.);
#1546=ADVANCED_FACE('',(#255),#184,.T.);
#1547=ADVANCED_FACE('',(#256),#1470,.T.);
#1548=ADVANCED_FACE('',(#257),#1471,.F.);
#1549=ADVANCED_FACE('',(#258),#1472,.T.);
#1550=ADVANCED_FACE('',(#259),#185,.T.);
#1551=ADVANCED_FACE('',(#260),#1473,.T.);
#1552=ADVANCED_FACE('',(#261),#1474,.F.);
#1553=ADVANCED_FACE('',(#262),#1475,.T.);
#1554=ADVANCED_FACE('',(#263),#186,.T.);
#1555=ADVANCED_FACE('',(#264),#1476,.T.);
#1556=ADVANCED_FACE('',(#265),#1477,.F.);
#1557=ADVANCED_FACE('',(#266),#131,.T.);
#1558=ADVANCED_FACE('',(#267),#132,.T.);
#1559=ADVANCED_FACE('',(#268),#133,.T.);
#1560=ADVANCED_FACE('',(#269),#134,.T.);
#1561=ADVANCED_FACE('',(#270),#135,.F.);
#1562=ADVANCED_FACE('',(#271),#136,.F.);
#1574=CLOSED_SHELL('',(#1482,#1483,#1484,#1485,#1486,#1487,#1488,#1489,
#1490,#1491,#1492,#1493,#1494,#1495,#1496,#1497,#1498,#1499,#1500,#1501,
#1502,#1503,#1504,#1505,#1506,#1507,#1508,#1509,#1510,#1511,#1512,#1513,
#1514,#1515,#1516,#1517,#1518,#1519,#1520,#1521,#1522,#1523,#1524,#1525,
#1526,#1527,#1528,#1529,#1530,#1531,#1532,#1533,#1534,#1535,#1536,#1537,
#1538,#1539,#1540,#1541,#1542,#1543,#1544,#1545,#1546,#1547,#1548,#1549,
#1550,#1551,#1552,#1553,#1554,#1555,#1556,#1557,#1558,#1559,#1560,#1561,
#1562));
#1624=AXIS2_PLACEMENT_3D('',#2306,#1820,#1821);
#1625=AXIS2_PLACEMENT_3D('',#2307,#1822,#1823);
#1626=AXIS2_PLACEMENT_3D('',#2309,#1824,#1825);
#1627=AXIS2_PLACEMENT_3D('',#2312,#1827,#1828);
#1628=AXIS2_PLACEMENT_3D('',#2313,#1829,#1830);
#1629=AXIS2_PLACEMENT_3D('',#2323,#1835,#1836);
#1630=AXIS2_PLACEMENT_3D('',#2324,#1837,#1838);
#1631=AXIS2_PLACEMENT_3D('',#2368,#1840,#1841);
#1632=AXIS2_PLACEMENT_3D('',#2370,#1842,#1843);
#1633=AXIS2_PLACEMENT_3D('',#2373,#1845,#1846);
#1634=AXIS2_PLACEMENT_3D('',#2374,#1847,#1848);
#1635=AXIS2_PLACEMENT_3D('',#2384,#1853,#1854);
#1636=AXIS2_PLACEMENT_3D('',#2385,#1855,#1856);
#1637=AXIS2_PLACEMENT_3D('',#2429,#1858,#1859);
#1638=AXIS2_PLACEMENT_3D('',#2432,#1861,#1862);
#1639=AXIS2_PLACEMENT_3D('',#2433,#1863,#1864);
#1640=AXIS2_PLACEMENT_3D('',#2477,#1866,#1867);
#1641=AXIS2_PLACEMENT_3D('',#2480,#1869,#1870);
#1642=AXIS2_PLACEMENT_3D('',#2481,#1871,#1872);
#1643=AXIS2_PLACEMENT_3D('',#2525,#1874,#1875);
#1644=AXIS2_PLACEMENT_3D('',#2527,#1876,#1877);
#1645=AXIS2_PLACEMENT_3D('',#2530,#1879,#1880);
#1646=AXIS2_PLACEMENT_3D('',#2531,#1881,#1882);
#1647=AXIS2_PLACEMENT_3D('',#2541,#1887,#1888);
#1648=AXIS2_PLACEMENT_3D('',#2542,#1889,#1890);
#1649=AXIS2_PLACEMENT_3D('',#2579,#1892,#1893);
#1650=AXIS2_PLACEMENT_3D('',#2581,#1894,#1895);
#1651=AXIS2_PLACEMENT_3D('',#2584,#1897,#1898);
#1652=AXIS2_PLACEMENT_3D('',#2585,#1899,#1900);
#1653=AXIS2_PLACEMENT_3D('',#2595,#1905,#1906);
#1654=AXIS2_PLACEMENT_3D('',#2596,#1907,#1908);
#1655=AXIS2_PLACEMENT_3D('',#2633,#1910,#1911);
#1656=AXIS2_PLACEMENT_3D('',#2636,#1913,#1914);
#1657=AXIS2_PLACEMENT_3D('',#2637,#1915,#1916);
#1658=AXIS2_PLACEMENT_3D('',#2674,#1918,#1919);
#1659=AXIS2_PLACEMENT_3D('',#2677,#1921,#1922);
#1660=AXIS2_PLACEMENT_3D('',#2678,#1923,#1924);
#1661=AXIS2_PLACEMENT_3D('',#2715,#1926,#1927);
#1662=AXIS2_PLACEMENT_3D('',#2797,#1929,#1930);
#1663=AXIS2_PLACEMENT_3D('',#2879,#1932,#1933);
#1664=AXIS2_PLACEMENT_3D('',#2961,#1935,#1936);
#1665=AXIS2_PLACEMENT_3D('',#3043,#1938,#1939);
#1666=AXIS2_PLACEMENT_3D('',#3045,#1940,#1941);
#1667=AXIS2_PLACEMENT_3D('',#3048,#1943,#1944);
#1668=AXIS2_PLACEMENT_3D('',#3049,#1945,#1946);
#1669=AXIS2_PLACEMENT_3D('',#3050,#1947,#1948);
#1670=AXIS2_PLACEMENT_3D('',#3052,#1949,#1950);
#1671=AXIS2_PLACEMENT_3D('',#3055,#1952,#1953);
#1672=AXIS2_PLACEMENT_3D('',#3056,#1954,#1955);
#1673=AXIS2_PLACEMENT_3D('',#3057,#1956,#1957);
#1674=AXIS2_PLACEMENT_3D('',#3059,#1958,#1959);
#1675=AXIS2_PLACEMENT_3D('',#3062,#1961,#1962);
#1676=AXIS2_PLACEMENT_3D('',#3063,#1963,#1964);
#1677=AXIS2_PLACEMENT_3D('',#3064,#1965,#1966);
#1678=AXIS2_PLACEMENT_3D('',#3066,#1967,#1968);
#1679=AXIS2_PLACEMENT_3D('',#3069,#1970,#1971);
#1680=AXIS2_PLACEMENT_3D('',#3070,#1972,#1973);
#1681=AXIS2_PLACEMENT_3D('',#3071,#1974,#1975);
#1682=AXIS2_PLACEMENT_3D('',#3077,#1979,#1980);
#1683=AXIS2_PLACEMENT_3D('',#3081,#1982,#1983);
#1684=AXIS2_PLACEMENT_3D('',#3082,#1984,#1985);
#1685=AXIS2_PLACEMENT_3D('',#3083,#1986,#1987);
#1686=AXIS2_PLACEMENT_3D('',#3085,#1988,#1989);
#1687=AXIS2_PLACEMENT_3D('',#3088,#1991,#1992);
#1688=AXIS2_PLACEMENT_3D('',#3089,#1993,#1994);
#1689=AXIS2_PLACEMENT_3D('',#3092,#1996,#1997);
#1690=AXIS2_PLACEMENT_3D('',#3093,#1998,#1999);
#1691=AXIS2_PLACEMENT_3D('',#3094,#2000,#2001);
#1692=AXIS2_PLACEMENT_3D('',#3098,#2004,#2005);
#1693=AXIS2_PLACEMENT_3D('',#3102,#2007,#2008);
#1694=AXIS2_PLACEMENT_3D('',#3103,#2009,#2010);
#1695=AXIS2_PLACEMENT_3D('',#3104,#2011,#2012);
#1696=AXIS2_PLACEMENT_3D('',#3106,#2013,#2014);
#1697=AXIS2_PLACEMENT_3D('',#3109,#2016,#2017);
#1698=AXIS2_PLACEMENT_3D('',#3110,#2018,#2019);
#1699=AXIS2_PLACEMENT_3D('',#3113,#2021,#2022);
#1700=AXIS2_PLACEMENT_3D('',#3114,#2023,#2024);
#1701=AXIS2_PLACEMENT_3D('',#3115,#2025,#2026);
#1702=AXIS2_PLACEMENT_3D('',#3119,#2029,#2030);
#1703=AXIS2_PLACEMENT_3D('',#3123,#2032,#2033);
#1704=AXIS2_PLACEMENT_3D('',#3124,#2034,#2035);
#1705=AXIS2_PLACEMENT_3D('',#3125,#2036,#2037);
#1706=AXIS2_PLACEMENT_3D('',#3127,#2038,#2039);
#1707=AXIS2_PLACEMENT_3D('',#3130,#2041,#2042);
#1708=AXIS2_PLACEMENT_3D('',#3131,#2043,#2044);
#1709=AXIS2_PLACEMENT_3D('',#3134,#2046,#2047);
#1710=AXIS2_PLACEMENT_3D('',#3135,#2048,#2049);
#1711=AXIS2_PLACEMENT_3D('',#3136,#2050,#2051);
#1712=AXIS2_PLACEMENT_3D('',#3140,#2054,#2055);
#1713=AXIS2_PLACEMENT_3D('',#3144,#2057,#2058);
#1714=AXIS2_PLACEMENT_3D('',#3145,#2059,#2060);
#1715=AXIS2_PLACEMENT_3D('',#3146,#2061,#2062);
#1716=AXIS2_PLACEMENT_3D('',#3148,#2063,#2064);
#1717=AXIS2_PLACEMENT_3D('',#3151,#2066,#2067);
#1718=AXIS2_PLACEMENT_3D('',#3152,#2068,#2069);
#1719=AXIS2_PLACEMENT_3D('',#3153,#2070,#2071);
#1720=AXIS2_PLACEMENT_3D('',#3154,#2072,#2073);
#1721=AXIS2_PLACEMENT_3D('',#3155,#2074,#2075);
#1722=AXIS2_PLACEMENT_3D('',#3158,#2077,#2078);
#1723=AXIS2_PLACEMENT_3D('',#3159,#2079,#2080);
#1724=AXIS2_PLACEMENT_3D('',#3162,#2082,#2083);
#1725=AXIS2_PLACEMENT_3D('',#3163,#2084,#2085);
#1726=AXIS2_PLACEMENT_3D('',#3164,#2086,#2087);
#1727=AXIS2_PLACEMENT_3D('',#3165,#2088,#2089);
#1728=AXIS2_PLACEMENT_3D('',#3168,#2091,#2092);
#1729=AXIS2_PLACEMENT_3D('',#3169,#2093,#2094);
#1730=AXIS2_PLACEMENT_3D('',#3172,#2096,#2097);
#1731=AXIS2_PLACEMENT_3D('',#3173,#2098,#2099);
#1732=AXIS2_PLACEMENT_3D('',#3174,#2100,#2101);
#1733=AXIS2_PLACEMENT_3D('',#3175,#2102,#2103);
#1734=AXIS2_PLACEMENT_3D('',#3177,#2104,#2105);
#1735=AXIS2_PLACEMENT_3D('',#3178,#2106,#2107);
#1736=AXIS2_PLACEMENT_3D('',#3180,#2108,#2109);
#1737=AXIS2_PLACEMENT_3D('',#3182,#2111,#2112);
#1738=AXIS2_PLACEMENT_3D('',#3184,#2113,#2114);
#1739=AXIS2_PLACEMENT_3D('',#3186,#2116,#2117);
#1740=AXIS2_PLACEMENT_3D('',#3188,#2118,#2119);
#1741=AXIS2_PLACEMENT_3D('',#3190,#2121,#2122);
#1742=AXIS2_PLACEMENT_3D('',#3193,#2123,#2124);
#1743=AXIS2_PLACEMENT_3D('',#3195,#2125,#2126);
#1744=AXIS2_PLACEMENT_3D('',#3197,#2127,#2128);
#1745=AXIS2_PLACEMENT_3D('',#3201,#2130,#2131);
#1746=AXIS2_PLACEMENT_3D('',#3203,#2132,#2133);
#1747=AXIS2_PLACEMENT_3D('',#3205,#2134,#2135);
#1748=AXIS2_PLACEMENT_3D('',#3209,#2137,#2138);
#1749=AXIS2_PLACEMENT_3D('',#3211,#2139,#2140);
#1750=AXIS2_PLACEMENT_3D('',#3213,#2141,#2142);
#1751=AXIS2_PLACEMENT_3D('',#3217,#2144,#2145);
#1752=AXIS2_PLACEMENT_3D('',#3219,#2146,#2147);
#1753=AXIS2_PLACEMENT_3D('',#3221,#2148,#2149);
#1754=AXIS2_PLACEMENT_3D('',#3223,#2151,#2152);
#1755=AXIS2_PLACEMENT_3D('',#3226,#2155,#2156);
#1756=AXIS2_PLACEMENT_3D('',#3228,#2158,#2159);
#1757=AXIS2_PLACEMENT_3D('',#3231,#2161,#2162);
#1758=AXIS2_PLACEMENT_3D('',#3232,#2163,#2164);
#1759=AXIS2_PLACEMENT_3D('',#3235,#2166,#2167);
#1760=AXIS2_PLACEMENT_3D('',#3236,#2168,#2169);
#1761=AXIS2_PLACEMENT_3D('',#3238,#2171,#2172);
#1762=AXIS2_PLACEMENT_3D('',#3239,#2173,#2174);
#1763=AXIS2_PLACEMENT_3D('',#3241,#2176,#2177);
#1764=AXIS2_PLACEMENT_3D('',#3244,#2179,#2180);
#1765=AXIS2_PLACEMENT_3D('',#3245,#2181,#2182);
#1766=AXIS2_PLACEMENT_3D('',#3248,#2184,#2185);
#1767=AXIS2_PLACEMENT_3D('',#3249,#2186,#2187);
#1768=AXIS2_PLACEMENT_3D('',#3251,#2189,#2190);
#1769=AXIS2_PLACEMENT_3D('',#3252,#2191,#2192);
#1770=AXIS2_PLACEMENT_3D('',#3254,#2194,#2195);
#1771=AXIS2_PLACEMENT_3D('',#3256,#2197,#2198);
#1772=AXIS2_PLACEMENT_3D('',#3258,#2200,#2201);
#1773=AXIS2_PLACEMENT_3D('',#3260,#2203,#2204);
#1774=AXIS2_PLACEMENT_3D('',#3262,#2206,#2207);
#1775=AXIS2_PLACEMENT_3D('',#3264,#2209,#2210);
#1776=AXIS2_PLACEMENT_3D('',#3265,#2211,#2212);
#1777=AXIS2_PLACEMENT_3D('',#3267,#2214,#2215);
#1778=AXIS2_PLACEMENT_3D('',#3269,#2217,#2218);
#1779=AXIS2_PLACEMENT_3D('',#3271,#2220,#2221);
#1780=AXIS2_PLACEMENT_3D('',#3273,#2223,#2224);
#1781=AXIS2_PLACEMENT_3D('',#3274,#2225,#2226);
#1820=DIRECTION('axis',(0.,0.,1.));
#1821=DIRECTION('refdir',(1.,0.,0.));
#1822=DIRECTION('center_axis',(1.,0.,0.));
#1823=DIRECTION('ref_axis',(0.,0.,-1.));
#1824=DIRECTION('center_axis',(1.,0.,0.));
#1825=DIRECTION('ref_axis',(0.,0.,-1.));
#1826=DIRECTION('',(-0.707106781186548,8.65956056235493E-17,-0.707106781186548));
#1827=DIRECTION('center_axis',(-1.,0.,0.));
#1828=DIRECTION('ref_axis',(0.,0.,-1.));
#1829=DIRECTION('center_axis',(1.,0.,0.));
#1830=DIRECTION('ref_axis',(0.,1.,0.));
#1831=DIRECTION('',(0.,-1.,0.));
#1832=DIRECTION('',(0.,0.,-1.));
#1833=DIRECTION('',(0.,1.,0.));
#1834=DIRECTION('',(0.,0.,1.));
#1835=DIRECTION('center_axis',(1.,0.,0.));
#1836=DIRECTION('ref_axis',(0.,0.,-1.));
#1837=DIRECTION('center_axis',(1.,0.,0.));
#1838=DIRECTION('ref_axis',(0.,0.,-1.));
#1839=DIRECTION('',(1.,0.,0.));
#1840=DIRECTION('center_axis',(-1.,0.,0.));
#1841=DIRECTION('ref_axis',(0.,0.,-1.));
#1842=DIRECTION('center_axis',(-1.,0.,0.));
#1843=DIRECTION('ref_axis',(0.,0.,-1.));
#1844=DIRECTION('',(0.707106781186548,-8.65956056235493E-17,-0.707106781186548));
#1845=DIRECTION('center_axis',(1.,0.,0.));
#1846=DIRECTION('ref_axis',(0.,0.,-1.));
#1847=DIRECTION('center_axis',(-1.,0.,0.));
#1848=DIRECTION('ref_axis',(0.,-1.,0.));
#1849=DIRECTION('',(0.,1.,0.));
#1850=DIRECTION('',(0.,0.,-1.));
#1851=DIRECTION('',(0.,-1.,0.));
#1852=DIRECTION('',(0.,0.,1.));
#1853=DIRECTION('center_axis',(-1.,0.,0.));
#1854=DIRECTION('ref_axis',(0.,0.,-1.));
#1855=DIRECTION('center_axis',(1.,0.,0.));
#1856=DIRECTION('ref_axis',(0.,0.,-1.));
#1857=DIRECTION('',(1.,0.,0.));
#1858=DIRECTION('center_axis',(1.,0.,0.));
#1859=DIRECTION('ref_axis',(0.,0.,-1.));
#1860=DIRECTION('',(-0.707106781186548,8.65956056235493E-17,-0.707106781186548));
#1861=DIRECTION('center_axis',(-1.,0.,0.));
#1862=DIRECTION('ref_axis',(0.,0.,-1.));
#1863=DIRECTION('center_axis',(1.,0.,0.));
#1864=DIRECTION('ref_axis',(0.,0.,-1.));
#1865=DIRECTION('',(1.,0.,0.));
#1866=DIRECTION('center_axis',(-1.,0.,0.));
#1867=DIRECTION('ref_axis',(0.,0.,-1.));
#1868=DIRECTION('',(0.707106781186548,-8.65956056235493E-17,-0.707106781186548));
#1869=DIRECTION('center_axis',(1.,0.,0.));
#1870=DIRECTION('ref_axis',(0.,0.,-1.));
#1871=DIRECTION('center_axis',(1.,0.,0.));
#1872=DIRECTION('ref_axis',(0.,0.,-1.));
#1873=DIRECTION('',(1.,0.,0.));
#1874=DIRECTION('center_axis',(0.,1.,0.));
#1875=DIRECTION('ref_axis',(1.,0.,0.));
#1876=DIRECTION('center_axis',(0.,1.,0.));
#1877=DIRECTION('ref_axis',(1.,0.,0.));
#1878=DIRECTION('',(0.707106781186548,-0.707106781186548,-8.65956056235493E-17));
#1879=DIRECTION('center_axis',(0.,-1.,0.));
#1880=DIRECTION('ref_axis',(1.,0.,0.));
#1881=DIRECTION('center_axis',(0.,1.,0.));
#1882=DIRECTION('ref_axis',(-1.,0.,0.));
#1883=DIRECTION('',(1.,0.,0.));
#1884=DIRECTION('',(0.,0.,-1.));
#1885=DIRECTION('',(-1.,0.,0.));
#1886=DIRECTION('',(0.,0.,1.));
#1887=DIRECTION('center_axis',(0.,1.,0.));
#1888=DIRECTION('ref_axis',(1.,0.,0.));
#1889=DIRECTION('center_axis',(0.,1.,0.));
#1890=DIRECTION('ref_axis',(1.,0.,0.));
#1891=DIRECTION('',(0.,1.,0.));
#1892=DIRECTION('center_axis',(0.,-1.,0.));
#1893=DIRECTION('ref_axis',(1.,0.,0.));
#1894=DIRECTION('center_axis',(0.,-1.,0.));
#1895=DIRECTION('ref_axis',(1.,0.,0.));
#1896=DIRECTION('',(0.707106781186548,0.707106781186548,8.65956056235493E-17));
#1897=DIRECTION('center_axis',(0.,1.,0.));
#1898=DIRECTION('ref_axis',(1.,0.,0.));
#1899=DIRECTION('center_axis',(0.,-1.,0.));
#1900=DIRECTION('ref_axis',(1.,0.,0.));
#1901=DIRECTION('',(-1.,0.,0.));
#1902=DIRECTION('',(0.,0.,-1.));
#1903=DIRECTION('',(1.,0.,0.));
#1904=DIRECTION('',(0.,0.,1.));
#1905=DIRECTION('center_axis',(0.,-1.,0.));
#1906=DIRECTION('ref_axis',(1.,0.,0.));
#1907=DIRECTION('center_axis',(0.,1.,0.));
#1908=DIRECTION('ref_axis',(1.,0.,0.));
#1909=DIRECTION('',(0.,1.,0.));
#1910=DIRECTION('center_axis',(0.,1.,0.));
#1911=DIRECTION('ref_axis',(1.,0.,0.));
#1912=DIRECTION('',(0.707106781186548,-0.707106781186548,-8.65956056235493E-17));
#1913=DIRECTION('center_axis',(0.,-1.,0.));
#1914=DIRECTION('ref_axis',(1.,0.,0.));
#1915=DIRECTION('center_axis',(0.,1.,0.));
#1916=DIRECTION('ref_axis',(1.,0.,0.));
#1917=DIRECTION('',(0.,1.,0.));
#1918=DIRECTION('center_axis',(0.,-1.,0.));
#1919=DIRECTION('ref_axis',(1.,0.,0.));
#1920=DIRECTION('',(0.707106781186548,0.707106781186548,8.65956056235493E-17));
#1921=DIRECTION('center_axis',(0.,1.,0.));
#1922=DIRECTION('ref_axis',(1.,0.,0.));
#1923=DIRECTION('center_axis',(0.,1.,0.));
#1924=DIRECTION('ref_axis',(1.,0.,0.));
#1925=DIRECTION('',(0.,1.,0.));
#1926=DIRECTION('center_axis',(1.,0.,0.));
#1927=DIRECTION('ref_axis',(0.,0.,-1.));
#1928=DIRECTION('',(1.,0.,0.));
#1929=DIRECTION('center_axis',(1.,0.,0.));
#1930=DIRECTION('ref_axis',(0.,0.,-1.));
#1931=DIRECTION('',(1.,0.,0.));
#1932=DIRECTION('center_axis',(1.,0.,0.));
#1933=DIRECTION('ref_axis',(0.,0.,-1.));
#1934=DIRECTION('',(1.,0.,0.));
#1935=DIRECTION('center_axis',(1.,0.,0.));
#1936=DIRECTION('ref_axis',(0.,0.,-1.));
#1937=DIRECTION('',(1.,0.,0.));
#1938=DIRECTION('center_axis',(0.,0.,1.));
#1939=DIRECTION('ref_axis',(0.,1.,0.));
#1940=DIRECTION('center_axis',(0.,0.,1.));
#1941=DIRECTION('ref_axis',(0.,1.,0.));
#1942=DIRECTION('',(0.,0.,1.));
#1943=DIRECTION('center_axis',(0.,0.,-1.));
#1944=DIRECTION('ref_axis',(0.,1.,0.));
#1945=DIRECTION('center_axis',(0.,0.,1.));
#1946=DIRECTION('ref_axis',(1.,0.,0.));
#1947=DIRECTION('center_axis',(0.,0.,1.));
#1948=DIRECTION('ref_axis',(0.,1.,0.));
#1949=DIRECTION('center_axis',(0.,0.,1.));
#1950=DIRECTION('ref_axis',(0.,1.,0.));
#1951=DIRECTION('',(0.,0.,1.));
#1952=DIRECTION('center_axis',(0.,0.,-1.));
#1953=DIRECTION('ref_axis',(0.,1.,0.));
#1954=DIRECTION('center_axis',(0.,0.,1.));
#1955=DIRECTION('ref_axis',(1.,0.,0.));
#1956=DIRECTION('center_axis',(0.,0.,1.));
#1957=DIRECTION('ref_axis',(1.,0.,0.));
#1958=DIRECTION('center_axis',(0.,0.,1.));
#1959=DIRECTION('ref_axis',(1.,0.,0.));
#1960=DIRECTION('',(0.,0.,1.));
#1961=DIRECTION('center_axis',(0.,0.,-1.));
#1962=DIRECTION('ref_axis',(1.,0.,0.));
#1963=DIRECTION('center_axis',(0.,0.,1.));
#1964=DIRECTION('ref_axis',(1.,0.,0.));
#1965=DIRECTION('center_axis',(0.,0.,1.));
#1966=DIRECTION('ref_axis',(1.,0.,0.));
#1967=DIRECTION('center_axis',(0.,0.,1.));
#1968=DIRECTION('ref_axis',(1.,0.,0.));
#1969=DIRECTION('',(0.,0.,1.));
#1970=DIRECTION('center_axis',(0.,0.,-1.));
#1971=DIRECTION('ref_axis',(1.,0.,0.));
#1972=DIRECTION('center_axis',(0.,0.,1.));
#1973=DIRECTION('ref_axis',(1.,0.,0.));
#1974=DIRECTION('center_axis',(0.,-0.707106781186547,-0.707106781186548));
#1975=DIRECTION('ref_axis',(-1.,0.,0.));
#1976=DIRECTION('',(-1.96261557335472E-15,-0.707106781186548,0.707106781186547));
#1977=DIRECTION('',(0.,0.707106781186548,-0.707106781186547));
#1978=DIRECTION('',(1.,0.,0.));
#1979=DIRECTION('center_axis',(0.,0.,1.));
#1980=DIRECTION('ref_axis',(0.639511031159242,-0.768781920329584,0.));
#1981=DIRECTION('',(0.695290346079778,-0.128729696062163,0.707106781186551));
#1982=DIRECTION('center_axis',(0.,0.,-1.));
#1983=DIRECTION('ref_axis',(0.639511031159242,-0.768781920329584,0.));
#1984=DIRECTION('center_axis',(0.,0.,1.));
#1985=DIRECTION('ref_axis',(0.639511031159242,-0.768781920329584,0.));
#1986=DIRECTION('center_axis',(0.,0.,-1.));
#1987=DIRECTION('ref_axis',(-0.105607476635515,0.994407894618038,0.));
#1988=DIRECTION('center_axis',(0.,0.,-1.));
#1989=DIRECTION('ref_axis',(-0.105607476635515,0.994407894618038,0.));
#1990=DIRECTION('',(0.128729696062162,-0.695290346079783,0.707106781186546));
#1991=DIRECTION('center_axis',(0.,0.,1.));
#1992=DIRECTION('ref_axis',(-0.105607476635515,0.994407894618038,0.));
#1993=DIRECTION('center_axis',(0.,0.,1.));
#1994=DIRECTION('ref_axis',(0.768781920329583,-0.639511031159243,0.));
#1995=DIRECTION('',(0.707106781186548,0.,0.707106781186547));
#1996=DIRECTION('center_axis',(0.,0.,-1.));
#1997=DIRECTION('ref_axis',(0.768781920329583,-0.639511031159243,0.));
#1998=DIRECTION('center_axis',(0.,0.,1.));
#1999=DIRECTION('ref_axis',(0.768781920329583,-0.639511031159243,0.));
#2000=DIRECTION('center_axis',(0.707106781186547,0.,-0.707106781186548));
#2001=DIRECTION('ref_axis',(-0.707106781186548,0.,-0.707106781186547));
#2002=DIRECTION('',(0.707106781186548,0.,0.707106781186547));
#2003=DIRECTION('',(0.,1.,0.));
#2004=DIRECTION('center_axis',(0.,0.,1.));
#2005=DIRECTION('ref_axis',(0.768781920329583,0.639511031159243,0.));
#2006=DIRECTION('',(0.12872969606217,0.695290346079785,0.707106781186544));
#2007=DIRECTION('center_axis',(0.,0.,-1.));
#2008=DIRECTION('ref_axis',(0.768781920329583,0.639511031159243,0.));
#2009=DIRECTION('center_axis',(0.,0.,1.));
#2010=DIRECTION('ref_axis',(0.768781920329583,0.639511031159243,0.));
#2011=DIRECTION('center_axis',(0.,0.,-1.));
#2012=DIRECTION('ref_axis',(-0.994407894618038,-0.105607476635514,0.));
#2013=DIRECTION('center_axis',(0.,0.,-1.));
#2014=DIRECTION('ref_axis',(-0.994407894618038,-0.105607476635514,0.));
#2015=DIRECTION('',(0.695290346079784,0.12872969606217,0.707106781186545));
#2016=DIRECTION('center_axis',(0.,0.,1.));
#2017=DIRECTION('ref_axis',(-0.994407894618038,-0.105607476635514,0.));
#2018=DIRECTION('center_axis',(0.,0.,1.));
#2019=DIRECTION('ref_axis',(0.639511031159243,0.768781920329583,0.));
#2020=DIRECTION('',(0.,0.707106781186548,0.707106781186547));
#2021=DIRECTION('center_axis',(0.,0.,-1.));
#2022=DIRECTION('ref_axis',(0.639511031159243,0.768781920329583,0.));
#2023=DIRECTION('center_axis',(0.,0.,1.));
#2024=DIRECTION('ref_axis',(0.639511031159243,0.768781920329583,0.));
#2025=DIRECTION('center_axis',(0.,0.707106781186547,-0.707106781186548));
#2026=DIRECTION('ref_axis',(-1.,0.,0.));
#2027=DIRECTION('',(0.,0.707106781186548,0.707106781186547));
#2028=DIRECTION('',(-1.,0.,0.));
#2029=DIRECTION('center_axis',(0.,0.,1.));
#2030=DIRECTION('ref_axis',(-0.639511031159243,0.768781920329583,0.));
#2031=DIRECTION('',(-0.695290346079785,0.12872969606217,0.707106781186544));
#2032=DIRECTION('center_axis',(0.,0.,-1.));
#2033=DIRECTION('ref_axis',(-0.639511031159243,0.768781920329583,0.));
#2034=DIRECTION('center_axis',(0.,0.,1.));
#2035=DIRECTION('ref_axis',(-0.639511031159243,0.768781920329583,0.));
#2036=DIRECTION('center_axis',(0.,0.,-1.));
#2037=DIRECTION('ref_axis',(0.105607476635514,-0.994407894618038,0.));
#2038=DIRECTION('center_axis',(0.,0.,-1.));
#2039=DIRECTION('ref_axis',(0.105607476635514,-0.994407894618038,0.));
#2040=DIRECTION('',(-0.12872969606217,0.695290346079784,0.707106781186545));
#2041=DIRECTION('center_axis',(0.,0.,1.));
#2042=DIRECTION('ref_axis',(0.105607476635514,-0.994407894618038,0.));
#2043=DIRECTION('center_axis',(0.,0.,1.));
#2044=DIRECTION('ref_axis',(-0.768781920329583,0.639511031159243,0.));
#2045=DIRECTION('',(-0.707106781186548,0.,0.707106781186547));
#2046=DIRECTION('center_axis',(0.,0.,-1.));
#2047=DIRECTION('ref_axis',(-0.768781920329583,0.639511031159243,0.));
#2048=DIRECTION('center_axis',(0.,0.,1.));
#2049=DIRECTION('ref_axis',(-0.768781920329583,0.639511031159243,0.));
#2050=DIRECTION('center_axis',(-0.707106781186547,0.,-0.707106781186548));
#2051=DIRECTION('ref_axis',(-0.707106781186548,0.,0.707106781186547));
#2052=DIRECTION('',(-0.707106781186548,0.,0.707106781186547));
#2053=DIRECTION('',(0.,-1.,0.));
#2054=DIRECTION('center_axis',(0.,0.,1.));
#2055=DIRECTION('ref_axis',(-0.768781920329584,-0.639511031159242,0.));
#2056=DIRECTION('',(-0.128729696062163,-0.695290346079781,0.707106781186548));
#2057=DIRECTION('center_axis',(0.,0.,-1.));
#2058=DIRECTION('ref_axis',(-0.768781920329584,-0.639511031159242,0.));
#2059=DIRECTION('center_axis',(0.,0.,1.));
#2060=DIRECTION('ref_axis',(-0.768781920329584,-0.639511031159242,0.));
#2061=DIRECTION('center_axis',(0.,0.,-1.));
#2062=DIRECTION('ref_axis',(0.994407894618038,0.105607476635515,0.));
#2063=DIRECTION('center_axis',(0.,0.,-1.));
#2064=DIRECTION('ref_axis',(0.994407894618038,0.105607476635515,0.));
#2065=DIRECTION('',(-0.695290346079783,-0.128729696062162,0.707106781186546));
#2066=DIRECTION('center_axis',(0.,0.,1.));
#2067=DIRECTION('ref_axis',(0.994407894618038,0.105607476635515,0.));
#2068=DIRECTION('center_axis',(0.,0.,1.));
#2069=DIRECTION('ref_axis',(-0.639511031159243,-0.768781920329583,0.));
#2070=DIRECTION('center_axis',(0.,0.,-1.));
#2071=DIRECTION('ref_axis',(-0.639511031159243,-0.768781920329583,0.));
#2072=DIRECTION('center_axis',(0.,0.,1.));
#2073=DIRECTION('ref_axis',(-0.639511031159243,-0.768781920329583,0.));
#2074=DIRECTION('center_axis',(0.,0.,1.));
#2075=DIRECTION('ref_axis',(-0.639511031159243,0.768781920329583,0.));
#2076=DIRECTION('',(0.,0.,1.));
#2077=DIRECTION('center_axis',(0.,0.,1.));
#2078=DIRECTION('ref_axis',(-0.639511031159243,0.768781920329583,0.));
#2079=DIRECTION('center_axis',(0.,0.,1.));
#2080=DIRECTION('ref_axis',(0.105607476635514,-0.994407894618038,0.));
#2081=DIRECTION('',(0.,0.,-1.));
#2082=DIRECTION('center_axis',(0.,0.,-1.));
#2083=DIRECTION('ref_axis',(0.105607476635514,-0.994407894618038,0.));
#2084=DIRECTION('center_axis',(0.,0.,1.));
#2085=DIRECTION('ref_axis',(-0.768781920329583,0.639511031159243,0.));
#2086=DIRECTION('center_axis',(0.,0.,1.));
#2087=DIRECTION('ref_axis',(-0.768781920329583,0.639511031159243,0.));
#2088=DIRECTION('center_axis',(0.,0.,1.));
#2089=DIRECTION('ref_axis',(-0.768781920329584,-0.639511031159242,0.));
#2090=DIRECTION('',(0.,0.,1.));
#2091=DIRECTION('center_axis',(0.,0.,1.));
#2092=DIRECTION('ref_axis',(-0.768781920329584,-0.639511031159242,0.));
#2093=DIRECTION('center_axis',(0.,0.,1.));
#2094=DIRECTION('ref_axis',(0.994407894618038,0.105607476635515,0.));
#2095=DIRECTION('',(0.,0.,-1.));
#2096=DIRECTION('center_axis',(0.,0.,-1.));
#2097=DIRECTION('ref_axis',(0.994407894618038,0.105607476635515,0.));
#2098=DIRECTION('center_axis',(0.,0.,1.));
#2099=DIRECTION('ref_axis',(-0.639511031159243,-0.768781920329583,0.));
#2100=DIRECTION('center_axis',(0.,0.,1.));
#2101=DIRECTION('ref_axis',(-0.639511031159243,-0.768781920329583,0.));
#2102=DIRECTION('center_axis',(0.,0.,1.));
#2103=DIRECTION('ref_axis',(1.,0.,0.));
#2104=DIRECTION('center_axis',(0.,0.,-1.));
#2105=DIRECTION('ref_axis',(1.,0.,0.));
#2106=DIRECTION('center_axis',(0.,0.,-1.));
#2107=DIRECTION('ref_axis',(1.,0.,0.));
#2108=DIRECTION('center_axis',(0.,0.,1.));
#2109=DIRECTION('ref_axis',(1.,0.,0.));
#2110=DIRECTION('',(-0.707106781186548,-8.65956056235494E-17,-0.707106781186547));
#2111=DIRECTION('center_axis',(0.,0.,1.));
#2112=DIRECTION('ref_axis',(1.,0.,0.));
#2113=DIRECTION('center_axis',(0.,0.,-1.));
#2114=DIRECTION('ref_axis',(1.,0.,0.));
#2115=DIRECTION('',(0.,0.,-1.));
#2116=DIRECTION('center_axis',(0.,0.,1.));
#2117=DIRECTION('ref_axis',(1.,0.,0.));
#2118=DIRECTION('center_axis',(0.,0.,1.));
#2119=DIRECTION('ref_axis',(1.,0.,0.));
#2120=DIRECTION('',(0.707106781186548,8.65956056235494E-17,-0.707106781186547));
#2121=DIRECTION('center_axis',(0.,0.,1.));
#2122=DIRECTION('ref_axis',(1.,0.,0.));
#2123=DIRECTION('center_axis',(0.,0.,-1.));
#2124=DIRECTION('ref_axis',(-0.639511031159243,0.768781920329583,0.));
#2125=DIRECTION('center_axis',(0.,0.,1.));
#2126=DIRECTION('ref_axis',(0.105607476635514,-0.994407894618038,0.));
#2127=DIRECTION('center_axis',(0.,0.,-1.));
#2128=DIRECTION('ref_axis',(-0.768781920329583,0.639511031159243,0.));
#2129=DIRECTION('',(0.,1.,0.));
#2130=DIRECTION('center_axis',(0.,0.,-1.));
#2131=DIRECTION('ref_axis',(-0.768781920329584,-0.639511031159242,0.));
#2132=DIRECTION('center_axis',(0.,0.,1.));
#2133=DIRECTION('ref_axis',(0.994407894618038,0.105607476635515,0.));
#2134=DIRECTION('center_axis',(0.,0.,-1.));
#2135=DIRECTION('ref_axis',(-0.639511031159243,-0.768781920329583,0.));
#2136=DIRECTION('',(-1.,0.,0.));
#2137=DIRECTION('center_axis',(0.,0.,-1.));
#2138=DIRECTION('ref_axis',(0.639511031159242,-0.768781920329584,0.));
#2139=DIRECTION('center_axis',(0.,0.,1.));
#2140=DIRECTION('ref_axis',(-0.105607476635515,0.994407894618038,0.));
#2141=DIRECTION('center_axis',(0.,0.,-1.));
#2142=DIRECTION('ref_axis',(0.768781920329583,-0.639511031159243,0.));
#2143=DIRECTION('',(0.,-1.,0.));
#2144=DIRECTION('center_axis',(0.,0.,-1.));
#2145=DIRECTION('ref_axis',(0.768781920329583,0.639511031159243,0.));
#2146=DIRECTION('center_axis',(0.,0.,1.));
#2147=DIRECTION('ref_axis',(-0.994407894618038,-0.105607476635514,0.));
#2148=DIRECTION('center_axis',(0.,0.,-1.));
#2149=DIRECTION('ref_axis',(0.639511031159243,0.768781920329583,0.));
#2150=DIRECTION('',(1.,0.,0.));
#2151=DIRECTION('center_axis',(0.,0.,-1.));
#2152=DIRECTION('ref_axis',(-0.639511031159243,0.768781920329583,0.));
#2153=DIRECTION('',(0.,0.707106781186546,-0.707106781186549));
#2154=DIRECTION('',(0.695290346079782,-0.12872969606217,0.707106781186546));
#2155=DIRECTION('center_axis',(0.,0.707106781186547,0.707106781186548));
#2156=DIRECTION('ref_axis',(1.,0.,0.));
#2157=DIRECTION('',(0.,0.707106781186548,-0.707106781186547));
#2158=DIRECTION('center_axis',(0.,0.,-1.));
#2159=DIRECTION('ref_axis',(0.639511031159243,0.768781920329583,0.));
#2160=DIRECTION('',(0.695290346079781,0.128729696062166,-0.707106781186548));
#2161=DIRECTION('center_axis',(0.,0.,1.));
#2162=DIRECTION('ref_axis',(0.639511031159243,0.768781920329583,0.));
#2163=DIRECTION('center_axis',(0.,0.,1.));
#2164=DIRECTION('ref_axis',(-0.994407894618038,-0.105607476635514,0.));
#2165=DIRECTION('',(0.128729696062166,0.695290346079781,-0.707106781186548));
#2166=DIRECTION('center_axis',(0.,0.,-1.));
#2167=DIRECTION('ref_axis',(-0.994407894618038,-0.105607476635514,0.));
#2168=DIRECTION('center_axis',(0.,0.,-1.));
#2169=DIRECTION('ref_axis',(0.768781920329583,0.639511031159243,0.));
#2170=DIRECTION('',(0.707106781186546,0.,-0.707106781186549));
#2171=DIRECTION('center_axis',(0.,0.,1.));
#2172=DIRECTION('ref_axis',(0.768781920329583,0.639511031159243,0.));
#2173=DIRECTION('center_axis',(0.707106781186547,0.,0.707106781186548));
#2174=DIRECTION('ref_axis',(0.707106781186548,0.,-0.707106781186547));
#2175=DIRECTION('',(0.707106781186548,0.,-0.707106781186547));
#2176=DIRECTION('center_axis',(0.,0.,-1.));
#2177=DIRECTION('ref_axis',(0.768781920329583,-0.639511031159243,0.));
#2178=DIRECTION('',(0.128729696062166,-0.695290346079781,-0.707106781186548));
#2179=DIRECTION('center_axis',(0.,0.,1.));
#2180=DIRECTION('ref_axis',(0.768781920329583,-0.639511031159243,0.));
#2181=DIRECTION('center_axis',(0.,0.,1.));
#2182=DIRECTION('ref_axis',(-0.105607476635515,0.994407894618038,0.));
#2183=DIRECTION('',(0.695290346079777,-0.128729696062167,-0.707106781186552));
#2184=DIRECTION('center_axis',(0.,0.,-1.));
#2185=DIRECTION('ref_axis',(-0.105607476635515,0.994407894618038,0.));
#2186=DIRECTION('center_axis',(0.,0.,-1.));
#2187=DIRECTION('ref_axis',(0.639511031159242,-0.768781920329584,0.));
#2188=DIRECTION('',(0.,-0.707106781186548,-0.707106781186547));
#2189=DIRECTION('center_axis',(0.,0.,1.));
#2190=DIRECTION('ref_axis',(0.639511031159242,-0.768781920329584,0.));
#2191=DIRECTION('center_axis',(0.,-0.707106781186547,0.707106781186548));
#2192=DIRECTION('ref_axis',(1.,0.,0.));
#2193=DIRECTION('',(0.,-0.707106781186548,-0.707106781186547));
#2194=DIRECTION('center_axis',(0.,0.,-1.));
#2195=DIRECTION('ref_axis',(-0.639511031159243,-0.768781920329583,0.));
#2196=DIRECTION('',(-0.695290346079781,-0.128729696062166,-0.707106781186548));
#2197=DIRECTION('center_axis',(0.,0.,1.));
#2198=DIRECTION('ref_axis',(0.994407894618038,0.105607476635515,0.));
#2199=DIRECTION('',(-0.12872969606217,-0.695290346079783,-0.707106781186545));
#2200=DIRECTION('center_axis',(0.,0.,-1.));
#2201=DIRECTION('ref_axis',(-0.768781920329584,-0.639511031159242,0.));
#2202=DIRECTION('',(-0.707106781186548,0.,-0.707106781186547));
#2203=DIRECTION('center_axis',(-0.707106781186547,0.,0.707106781186548));
#2204=DIRECTION('ref_axis',(0.707106781186548,0.,0.707106781186547));
#2205=DIRECTION('',(-0.707106781186548,0.,-0.707106781186547));
#2206=DIRECTION('center_axis',(0.,0.,-1.));
#2207=DIRECTION('ref_axis',(-0.768781920329583,0.639511031159243,0.));
#2208=DIRECTION('',(-0.128729696062166,0.695290346079781,-0.707106781186548));
#2209=DIRECTION('center_axis',(0.,0.,1.));
#2210=DIRECTION('ref_axis',(0.105607476635514,-0.994407894618038,0.));
#2211=DIRECTION('center_axis',(0.,0.,1.));
#2212=DIRECTION('ref_axis',(0.639511031159242,-0.768781920329584,0.));
#2213=DIRECTION('',(0.,0.,1.));
#2214=DIRECTION('center_axis',(0.,0.,1.));
#2215=DIRECTION('ref_axis',(0.768781920329583,-0.639511031159243,0.));
#2216=DIRECTION('',(0.,0.,-1.));
#2217=DIRECTION('center_axis',(0.,0.,1.));
#2218=DIRECTION('ref_axis',(0.768781920329583,0.639511031159243,0.));
#2219=DIRECTION('',(0.,0.,1.));
#2220=DIRECTION('center_axis',(0.,0.,1.));
#2221=DIRECTION('ref_axis',(0.639511031159243,0.768781920329583,0.));
#2222=DIRECTION('',(0.,0.,-1.));
#2223=DIRECTION('center_axis',(0.,0.,1.));
#2224=DIRECTION('ref_axis',(-0.994407894618038,-0.105607476635514,0.));
#2225=DIRECTION('center_axis',(0.,0.,1.));
#2226=DIRECTION('ref_axis',(-0.105607476635515,0.994407894618038,0.));
#2306=CARTESIAN_POINT('',(0.,0.,0.));
#2307=CARTESIAN_POINT('Origin',(26.9,-2.,5.3));
#2308=CARTESIAN_POINT('',(27.,-2.,6.75));
#2309=CARTESIAN_POINT('Origin',(27.,-2.,5.3));
#2310=CARTESIAN_POINT('',(26.8,-2.,6.55));
#2311=CARTESIAN_POINT('',(26.9,-2.,6.65));
#2312=CARTESIAN_POINT('Origin',(26.8,-2.,5.3));
#2313=CARTESIAN_POINT('Origin',(27.,-7.97967105517398,0.));
#2314=CARTESIAN_POINT('',(27.,6.25103652921323,0.4));
#2315=CARTESIAN_POINT('',(27.,-6.25103652921323,0.4));
#2316=CARTESIAN_POINT('',(27.,-3.98983552758699,0.4));
#2317=CARTESIAN_POINT('',(27.,6.25103652921323,8.2));
#2318=CARTESIAN_POINT('',(27.,6.25103652921323,0.));
#2319=CARTESIAN_POINT('',(27.,-6.25103652921323,8.2));
#2320=CARTESIAN_POINT('',(27.,-3.98983552758699,8.2));
#2321=CARTESIAN_POINT('',(27.,-6.25103652921323,0.));
#2322=CARTESIAN_POINT('',(27.,2.,6.75));
#2323=CARTESIAN_POINT('Origin',(27.,2.,5.3));
#2324=CARTESIAN_POINT('Origin',(0.,-2.,5.3));
#2325=CARTESIAN_POINT('',(24.9186985827943,-0.75,5.3));
#2326=CARTESIAN_POINT('',(24.372281323269,-2.,6.55));
#2327=CARTESIAN_POINT('Ctrl Pts',(24.9186985827943,-0.75,5.3));
#2328=CARTESIAN_POINT('Ctrl Pts',(24.9186985827943,-0.75,5.45557706538823));
#2329=CARTESIAN_POINT('Ctrl Pts',(24.9123746835565,-0.780900542172469,5.62135879792505));
#2330=CARTESIAN_POINT('Ctrl Pts',(24.8815010802748,-0.905294021223847,5.92537474512899));
#2331=CARTESIAN_POINT('Ctrl Pts',(24.8563182098205,-0.998771663818447,6.06355058537597));
#2332=CARTESIAN_POINT('Ctrl Pts',(24.78127088064,-1.22443201701213,6.29525819606588));
#2333=CARTESIAN_POINT('Ctrl Pts',(24.7232785375987,-1.37524312511396,6.39595782382434));
#2334=CARTESIAN_POINT('Ctrl Pts',(24.5694895702423,-1.69087323617109,6.52306381241391));
#2335=CARTESIAN_POINT('Ctrl Pts',(24.4731108768197,-1.85519457825137,6.55));
#2336=CARTESIAN_POINT('Ctrl Pts',(24.372281323269,-2.,6.55));
#2337=CARTESIAN_POINT('Ctrl Pts',(24.372281323269,-2.,6.55));
#2338=CARTESIAN_POINT('Ctrl Pts',(24.2385424047286,-2.19206789895891,6.55));
#2339=CARTESIAN_POINT('Ctrl Pts',(24.0765750988521,-2.38072616471554,6.50435864359466));
#2340=CARTESIAN_POINT('Ctrl Pts',(23.7307236627921,-2.70748360064366,6.34637446065785));
#2341=CARTESIAN_POINT('Ctrl Pts',(23.5468663875633,-2.84596078128561,6.23475573757803));
#2342=CARTESIAN_POINT('Ctrl Pts',(23.2511744930699,-3.03425420344229,6.01333284729064));
#2343=CARTESIAN_POINT('Ctrl Pts',(23.1129712312086,-3.10865620052542,5.89516586902311));
#2344=CARTESIAN_POINT('Ctrl Pts',(22.9447171723108,-3.18851767079192,5.69387466967946));
#2345=CARTESIAN_POINT('Ctrl Pts',(22.8954952065846,-3.2100076151372,5.62308391879915));
#2346=CARTESIAN_POINT('Ctrl Pts',(22.8227994048359,-3.24064153091951,5.47120219564432));
#2347=CARTESIAN_POINT('Ctrl Pts',(22.7990381056767,-3.25,5.39029234212096));
#2348=CARTESIAN_POINT('Ctrl Pts',(22.7990381056767,-3.25,5.20970765787903));
#2349=CARTESIAN_POINT('Ctrl Pts',(22.8227994048359,-3.24064153091951,5.12879780435568));
#2350=CARTESIAN_POINT('Ctrl Pts',(22.8954952065846,-3.2100076151372,4.97691608120085));
#2351=CARTESIAN_POINT('Ctrl Pts',(22.9447171723108,-3.18851767079192,4.90612533032054));
#2352=CARTESIAN_POINT('Ctrl Pts',(23.1129712312086,-3.10865620052542,4.70483413097689));
#2353=CARTESIAN_POINT('Ctrl Pts',(23.2511744930699,-3.03425420344229,4.58666715270936));
#2354=CARTESIAN_POINT('Ctrl Pts',(23.5468663875633,-2.84596078128561,4.36524426242197));
#2355=CARTESIAN_POINT('Ctrl Pts',(23.7307236627921,-2.70748360064366,4.25362553934216));
#2356=CARTESIAN_POINT('Ctrl Pts',(24.0765750988521,-2.38072616471554,4.09564135640534));
#2357=CARTESIAN_POINT('Ctrl Pts',(24.2385424047286,-2.19206789895891,4.05));
#2358=CARTESIAN_POINT('Ctrl Pts',(24.4731108768197,-1.85519457825137,4.05));
#2359=CARTESIAN_POINT('Ctrl Pts',(24.5694895702423,-1.69087323617109,4.07693618758609));
#2360=CARTESIAN_POINT('Ctrl Pts',(24.7232785375987,-1.37524312511396,4.20404217617566));
#2361=CARTESIAN_POINT('Ctrl Pts',(24.7812708806401,-1.22443201701213,4.30474180393412));
#2362=CARTESIAN_POINT('Ctrl Pts',(24.8563182098205,-0.998771663818447,4.53644941462403));
#2363=CARTESIAN_POINT('Ctrl Pts',(24.8815010802748,-0.905294021223847,4.67462525487101));
#2364=CARTESIAN_POINT('Ctrl Pts',(24.9123746835565,-0.780900542172468,4.97864120207495));
#2365=CARTESIAN_POINT('Ctrl Pts',(24.9186985827943,-0.75,5.14442293461177));
#2366=CARTESIAN_POINT('Ctrl Pts',(24.9186985827943,-0.75,5.3));
#2367=CARTESIAN_POINT('',(0.,-2.,6.55));
#2368=CARTESIAN_POINT('Origin',(-26.9,-2.,5.3));
#2369=CARTESIAN_POINT('',(-27.,-2.,6.75));
#2370=CARTESIAN_POINT('Origin',(-27.,-2.,5.3));
#2371=CARTESIAN_POINT('',(-26.8,-2.,6.55));
#2372=CARTESIAN_POINT('',(-26.9,-2.,6.65));
#2373=CARTESIAN_POINT('Origin',(-26.8,-2.,5.3));
#2374=CARTESIAN_POINT('Origin',(-27.,7.97967105517399,0.));
#2375=CARTESIAN_POINT('',(-27.,-6.25103652921323,0.4));
#2376=CARTESIAN_POINT('',(-27.,6.25103652921323,0.4));
#2377=CARTESIAN_POINT('',(-27.,3.98983552758699,0.4));
#2378=CARTESIAN_POINT('',(-27.,-6.25103652921323,8.2));
#2379=CARTESIAN_POINT('',(-27.,-6.25103652921323,0.));
#2380=CARTESIAN_POINT('',(-27.,6.25103652921323,8.2));
#2381=CARTESIAN_POINT('',(-27.,3.98983552758699,8.2));
#2382=CARTESIAN_POINT('',(-27.,6.25103652921323,0.));
#2383=CARTESIAN_POINT('',(-27.,2.,6.75));
#2384=CARTESIAN_POINT('Origin',(-27.,2.,5.3));
#2385=CARTESIAN_POINT('Origin',(0.,-2.,5.3));
#2386=CARTESIAN_POINT('',(-24.372281323269,-2.,6.55));
#2387=CARTESIAN_POINT('',(0.,-2.,6.55));
#2388=CARTESIAN_POINT('',(-24.9186985827943,-0.75,5.3));
#2389=CARTESIAN_POINT('Ctrl Pts',(-24.9186985827943,-0.75,5.3));
#2390=CARTESIAN_POINT('Ctrl Pts',(-24.9186985827943,-0.75,5.14442293461177));
#2391=CARTESIAN_POINT('Ctrl Pts',(-24.9123746835565,-0.780900542172468,
4.97864120207495));
#2392=CARTESIAN_POINT('Ctrl Pts',(-24.8815010802748,-0.905294021223847,
4.67462525487101));
#2393=CARTESIAN_POINT('Ctrl Pts',(-24.8563182098205,-0.998771663818447,
4.53644941462403));
#2394=CARTESIAN_POINT('Ctrl Pts',(-24.78127088064,-1.22443201701213,4.30474180393412));
#2395=CARTESIAN_POINT('Ctrl Pts',(-24.7232785375987,-1.37524312511397,4.20404217617566));
#2396=CARTESIAN_POINT('Ctrl Pts',(-24.5694895702423,-1.69087323617109,4.07693618758609));
#2397=CARTESIAN_POINT('Ctrl Pts',(-24.4731108768197,-1.85519457825137,4.05));
#2398=CARTESIAN_POINT('Ctrl Pts',(-24.2385424047286,-2.19206789895891,4.05));
#2399=CARTESIAN_POINT('Ctrl Pts',(-24.0765750988521,-2.38072616471554,4.09564135640534));
#2400=CARTESIAN_POINT('Ctrl Pts',(-23.7307236627921,-2.70748360064366,4.25362553934216));
#2401=CARTESIAN_POINT('Ctrl Pts',(-23.5468663875633,-2.84596078128561,4.36524426242197));
#2402=CARTESIAN_POINT('Ctrl Pts',(-23.2511744930699,-3.03425420344229,4.58666715270936));
#2403=CARTESIAN_POINT('Ctrl Pts',(-23.1129712312086,-3.10865620052542,4.70483413097689));
#2404=CARTESIAN_POINT('Ctrl Pts',(-22.9447171723108,-3.18851767079192,4.90612533032054));
#2405=CARTESIAN_POINT('Ctrl Pts',(-22.8954952065846,-3.2100076151372,4.97691608120085));
#2406=CARTESIAN_POINT('Ctrl Pts',(-22.8227994048359,-3.24064153091951,5.12879780435568));
#2407=CARTESIAN_POINT('Ctrl Pts',(-22.7990381056767,-3.25,5.20970765787904));
#2408=CARTESIAN_POINT('Ctrl Pts',(-22.7990381056767,-3.25,5.39029234212096));
#2409=CARTESIAN_POINT('Ctrl Pts',(-22.8227994048359,-3.24064153091951,5.47120219564432));
#2410=CARTESIAN_POINT('Ctrl Pts',(-22.8954952065846,-3.2100076151372,5.62308391879915));
#2411=CARTESIAN_POINT('Ctrl Pts',(-22.9447171723108,-3.18851767079192,5.69387466967946));
#2412=CARTESIAN_POINT('Ctrl Pts',(-23.1129712312086,-3.10865620052542,5.89516586902311));
#2413=CARTESIAN_POINT('Ctrl Pts',(-23.2511744930699,-3.03425420344229,6.01333284729064));
#2414=CARTESIAN_POINT('Ctrl Pts',(-23.5468663875633,-2.84596078128561,6.23475573757803));
#2415=CARTESIAN_POINT('Ctrl Pts',(-23.7307236627921,-2.70748360064366,6.34637446065785));
#2416=CARTESIAN_POINT('Ctrl Pts',(-24.0765750988521,-2.38072616471554,6.50435864359466));
#2417=CARTESIAN_POINT('Ctrl Pts',(-24.2385424047286,-2.19206789895891,6.55));
#2418=CARTESIAN_POINT('Ctrl Pts',(-24.372281323269,-2.,6.55));
#2419=CARTESIAN_POINT('Ctrl Pts',(-24.372281323269,-2.,6.55));
#2420=CARTESIAN_POINT('Ctrl Pts',(-24.4731108768197,-1.85519457825137,6.55));
#2421=CARTESIAN_POINT('Ctrl Pts',(-24.5694895702423,-1.69087323617109,6.52306381241391));
#2422=CARTESIAN_POINT('Ctrl Pts',(-24.7232785375987,-1.37524312511397,6.39595782382434));
#2423=CARTESIAN_POINT('Ctrl Pts',(-24.78127088064,-1.22443201701213,6.29525819606588));
#2424=CARTESIAN_POINT('Ctrl Pts',(-24.8563182098205,-0.998771663818447,
6.06355058537597));
#2425=CARTESIAN_POINT('Ctrl Pts',(-24.8815010802748,-0.905294021223847,
5.92537474512899));
#2426=CARTESIAN_POINT('Ctrl Pts',(-24.9123746835565,-0.780900542172469,
5.62135879792505));
#2427=CARTESIAN_POINT('Ctrl Pts',(-24.9186985827943,-0.75,5.45557706538823));
#2428=CARTESIAN_POINT('Ctrl Pts',(-24.9186985827943,-0.75,5.3));
#2429=CARTESIAN_POINT('Origin',(26.9,2.,5.3));
#2430=CARTESIAN_POINT('',(26.8,2.,6.55));
#2431=CARTESIAN_POINT('',(26.9,2.,6.65));
#2432=CARTESIAN_POINT('Origin',(26.8,2.,5.3));
#2433=CARTESIAN_POINT('Origin',(0.,2.,5.3));
#2434=CARTESIAN_POINT('',(22.7990381056767,3.25,5.3));
#2435=CARTESIAN_POINT('',(24.372281323269,2.,6.55));
#2436=CARTESIAN_POINT('Ctrl Pts',(22.7990381056767,3.25,5.3));
#2437=CARTESIAN_POINT('Ctrl Pts',(22.7990381056767,3.25,5.39029234212097));
#2438=CARTESIAN_POINT('Ctrl Pts',(22.8227994048359,3.24064153091951,5.47120219564433));
#2439=CARTESIAN_POINT('Ctrl Pts',(22.8954952065846,3.2100076151372,5.62308391879915));
#2440=CARTESIAN_POINT('Ctrl Pts',(22.9447171723108,3.18851767079192,5.69387466967946));
#2441=CARTESIAN_POINT('Ctrl Pts',(23.1129712312086,3.10865620052542,5.89516586902311));
#2442=CARTESIAN_POINT('Ctrl Pts',(23.2511744930699,3.03425420344229,6.01333284729064));
#2443=CARTESIAN_POINT('Ctrl Pts',(23.5468663875633,2.84596078128561,6.23475573757803));
#2444=CARTESIAN_POINT('Ctrl Pts',(23.7307236627921,2.70748360064366,6.34637446065785));
#2445=CARTESIAN_POINT('Ctrl Pts',(24.0765750988521,2.38072616471554,6.50435864359466));
#2446=CARTESIAN_POINT('Ctrl Pts',(24.2385424047286,2.19206789895891,6.55));
#2447=CARTESIAN_POINT('Ctrl Pts',(24.372281323269,2.,6.55));
#2448=CARTESIAN_POINT('Ctrl Pts',(24.372281323269,2.,6.55));
#2449=CARTESIAN_POINT('Ctrl Pts',(24.4731108768197,1.85519457825136,6.55));
#2450=CARTESIAN_POINT('Ctrl Pts',(24.5694895702423,1.69087323617109,6.52306381241391));
#2451=CARTESIAN_POINT('Ctrl Pts',(24.7232785375987,1.37524312511396,6.39595782382434));
#2452=CARTESIAN_POINT('Ctrl Pts',(24.7812708806401,1.22443201701213,6.29525819606588));
#2453=CARTESIAN_POINT('Ctrl Pts',(24.8563182098205,0.998771663818447,6.06355058537597));
#2454=CARTESIAN_POINT('Ctrl Pts',(24.8815010802748,0.905294021223848,5.92537474512899));
#2455=CARTESIAN_POINT('Ctrl Pts',(24.9123746835565,0.780900542172469,5.62135879792505));
#2456=CARTESIAN_POINT('Ctrl Pts',(24.9186985827943,0.75,5.45557706538823));
#2457=CARTESIAN_POINT('Ctrl Pts',(24.9186985827943,0.75,5.14442293461177));
#2458=CARTESIAN_POINT('Ctrl Pts',(24.9123746835565,0.780900542172469,4.97864120207495));
#2459=CARTESIAN_POINT('Ctrl Pts',(24.8815010802748,0.905294021223848,4.67462525487101));
#2460=CARTESIAN_POINT('Ctrl Pts',(24.8563182098205,0.998771663818447,4.53644941462403));
#2461=CARTESIAN_POINT('Ctrl Pts',(24.78127088064,1.22443201701213,4.30474180393412));
#2462=CARTESIAN_POINT('Ctrl Pts',(24.7232785375987,1.37524312511397,4.20404217617566));
#2463=CARTESIAN_POINT('Ctrl Pts',(24.5694895702423,1.69087323617109,4.07693618758609));
#2464=CARTESIAN_POINT('Ctrl Pts',(24.4731108768197,1.85519457825137,4.05));
#2465=CARTESIAN_POINT('Ctrl Pts',(24.2385424047286,2.19206789895891,4.05));
#2466=CARTESIAN_POINT('Ctrl Pts',(24.0765750988521,2.38072616471554,4.09564135640534));
#2467=CARTESIAN_POINT('Ctrl Pts',(23.7307236627921,2.70748360064366,4.25362553934216));
#2468=CARTESIAN_POINT('Ctrl Pts',(23.5468663875633,2.84596078128561,4.36524426242197));
#2469=CARTESIAN_POINT('Ctrl Pts',(23.2511744930699,3.03425420344229,4.58666715270936));
#2470=CARTESIAN_POINT('Ctrl Pts',(23.1129712312086,3.10865620052542,4.70483413097689));
#2471=CARTESIAN_POINT('Ctrl Pts',(22.9447171723108,3.18851767079192,4.90612533032054));
#2472=CARTESIAN_POINT('Ctrl Pts',(22.8954952065846,3.2100076151372,4.97691608120085));
#2473=CARTESIAN_POINT('Ctrl Pts',(22.8227994048359,3.24064153091951,5.12879780435568));
#2474=CARTESIAN_POINT('Ctrl Pts',(22.7990381056767,3.25,5.20970765787903));
#2475=CARTESIAN_POINT('Ctrl Pts',(22.7990381056767,3.25,5.3));
#2476=CARTESIAN_POINT('',(0.,2.,6.55));
#2477=CARTESIAN_POINT('Origin',(-26.9,2.,5.3));
#2478=CARTESIAN_POINT('',(-26.8,2.,6.55));
#2479=CARTESIAN_POINT('',(-26.9,2.,6.65));
#2480=CARTESIAN_POINT('Origin',(-26.8,2.,5.3));
#2481=CARTESIAN_POINT('Origin',(0.,2.,5.3));
#2482=CARTESIAN_POINT('',(-24.372281323269,2.,6.55));
#2483=CARTESIAN_POINT('',(0.,2.,6.55));
#2484=CARTESIAN_POINT('',(-22.7990381056767,3.25,5.3));
#2485=CARTESIAN_POINT('Ctrl Pts',(-22.7990381056767,3.25,5.3));
#2486=CARTESIAN_POINT('Ctrl Pts',(-22.7990381056767,3.25,5.20970765787904));
#2487=CARTESIAN_POINT('Ctrl Pts',(-22.8227994048359,3.24064153091951,5.12879780435568));
#2488=CARTESIAN_POINT('Ctrl Pts',(-22.8954952065846,3.2100076151372,4.97691608120085));
#2489=CARTESIAN_POINT('Ctrl Pts',(-22.9447171723108,3.18851767079192,4.90612533032054));
#2490=CARTESIAN_POINT('Ctrl Pts',(-23.1129712312086,3.10865620052542,4.70483413097689));
#2491=CARTESIAN_POINT('Ctrl Pts',(-23.2511744930699,3.03425420344229,4.58666715270936));
#2492=CARTESIAN_POINT('Ctrl Pts',(-23.5468663875633,2.84596078128561,4.36524426242197));
#2493=CARTESIAN_POINT('Ctrl Pts',(-23.7307236627921,2.70748360064366,4.25362553934216));
#2494=CARTESIAN_POINT('Ctrl Pts',(-24.0765750988521,2.38072616471554,4.09564135640534));
#2495=CARTESIAN_POINT('Ctrl Pts',(-24.2385424047286,2.19206789895891,4.05));
#2496=CARTESIAN_POINT('Ctrl Pts',(-24.4731108768197,1.85519457825137,4.05));
#2497=CARTESIAN_POINT('Ctrl Pts',(-24.5694895702423,1.69087323617109,4.07693618758609));
#2498=CARTESIAN_POINT('Ctrl Pts',(-24.7232785375987,1.37524312511396,4.20404217617566));
#2499=CARTESIAN_POINT('Ctrl Pts',(-24.7812708806401,1.22443201701213,4.30474180393412));
#2500=CARTESIAN_POINT('Ctrl Pts',(-24.8563182098205,0.998771663818447,4.53644941462403));
#2501=CARTESIAN_POINT('Ctrl Pts',(-24.8815010802748,0.905294021223848,4.67462525487101));
#2502=CARTESIAN_POINT('Ctrl Pts',(-24.9123746835565,0.780900542172469,4.97864120207495));
#2503=CARTESIAN_POINT('Ctrl Pts',(-24.9186985827943,0.75,5.14442293461177));
#2504=CARTESIAN_POINT('Ctrl Pts',(-24.9186985827943,0.75,5.45557706538823));
#2505=CARTESIAN_POINT('Ctrl Pts',(-24.9123746835565,0.780900542172468,5.62135879792505));
#2506=CARTESIAN_POINT('Ctrl Pts',(-24.8815010802748,0.905294021223847,5.92537474512899));
#2507=CARTESIAN_POINT('Ctrl Pts',(-24.8563182098205,0.998771663818447,6.06355058537597));
#2508=CARTESIAN_POINT('Ctrl Pts',(-24.7812708806401,1.22443201701213,6.29525819606588));
#2509=CARTESIAN_POINT('Ctrl Pts',(-24.7232785375987,1.37524312511396,6.39595782382434));
#2510=CARTESIAN_POINT('Ctrl Pts',(-24.5694895702423,1.69087323617109,6.52306381241391));
#2511=CARTESIAN_POINT('Ctrl Pts',(-24.4731108768197,1.85519457825136,6.55));
#2512=CARTESIAN_POINT('Ctrl Pts',(-24.372281323269,2.,6.55));
#2513=CARTESIAN_POINT('Ctrl Pts',(-24.372281323269,2.,6.55));
#2514=CARTESIAN_POINT('Ctrl Pts',(-24.2385424047286,2.19206789895891,6.55));
#2515=CARTESIAN_POINT('Ctrl Pts',(-24.0765750988521,2.38072616471554,6.50435864359466));
#2516=CARTESIAN_POINT('Ctrl Pts',(-23.7307236627921,2.70748360064366,6.34637446065785));
#2517=CARTESIAN_POINT('Ctrl Pts',(-23.5468663875633,2.84596078128561,6.23475573757803));
#2518=CARTESIAN_POINT('Ctrl Pts',(-23.2511744930699,3.03425420344229,6.01333284729064));
#2519=CARTESIAN_POINT('Ctrl Pts',(-23.1129712312086,3.10865620052542,5.89516586902311));
#2520=CARTESIAN_POINT('Ctrl Pts',(-22.9447171723108,3.18851767079192,5.69387466967946));
#2521=CARTESIAN_POINT('Ctrl Pts',(-22.8954952065846,3.2100076151372,5.62308391879915));
#2522=CARTESIAN_POINT('Ctrl Pts',(-22.8227994048359,3.24064153091951,5.47120219564432));
#2523=CARTESIAN_POINT('Ctrl Pts',(-22.7990381056767,3.25,5.39029234212096));
#2524=CARTESIAN_POINT('Ctrl Pts',(-22.7990381056767,3.25,5.3));
#2525=CARTESIAN_POINT('Origin',(-2.,26.9,5.3));
#2526=CARTESIAN_POINT('',(-3.45,27.,5.3));
#2527=CARTESIAN_POINT('Origin',(-2.,27.,5.3));
#2528=CARTESIAN_POINT('',(-3.25,26.8,5.3));
#2529=CARTESIAN_POINT('',(-3.35,26.9,5.3));
#2530=CARTESIAN_POINT('Origin',(-2.,26.8,5.3));
#2531=CARTESIAN_POINT('Origin',(7.97967105517399,27.,0.));
#2532=CARTESIAN_POINT('',(-6.25103652921323,27.,0.4));
#2533=CARTESIAN_POINT('',(6.25103652921323,27.,0.4));
#2534=CARTESIAN_POINT('',(3.98983552758699,27.,0.4));
#2535=CARTESIAN_POINT('',(-6.25103652921323,27.,8.2));
#2536=CARTESIAN_POINT('',(-6.25103652921323,27.,0.));
#2537=CARTESIAN_POINT('',(6.25103652921323,27.,8.2));
#2538=CARTESIAN_POINT('',(3.98983552758699,27.,8.2));
#2539=CARTESIAN_POINT('',(6.25103652921323,27.,0.));
#2540=CARTESIAN_POINT('',(0.55,27.,5.3));
#2541=CARTESIAN_POINT('Origin',(2.,27.,5.3));
#2542=CARTESIAN_POINT('Origin',(-2.,0.,5.3));
#2543=CARTESIAN_POINT('',(-3.25,13.1029576813787,5.3));
#2544=CARTESIAN_POINT('Ctrl Pts',(-3.25,13.1029576813787,5.3));
#2545=CARTESIAN_POINT('Ctrl Pts',(-3.25,13.1029576813787,5.45705900752669));
#2546=CARTESIAN_POINT('Ctrl Pts',(-3.21857778155664,13.1108737267815,5.6242083709253));
#2547=CARTESIAN_POINT('Ctrl Pts',(-3.09176308346025,13.1413566197491,5.93094872999216));
#2548=CARTESIAN_POINT('Ctrl Pts',(-2.99640130889512,13.163742383297,6.07057038726816));
#2549=CARTESIAN_POINT('Ctrl Pts',(-2.77577516736032,13.2120416331141,6.29277806157361));
#2550=CARTESIAN_POINT('Ctrl Pts',(-2.6349594886099,13.2412866081987,6.38963814030342));
#2551=CARTESIAN_POINT('Ctrl Pts',(-2.32609557960331,13.2990210880236,6.51825552186166));
#2552=CARTESIAN_POINT('Ctrl Pts',(-2.15801374389282,13.3273592779611,6.55));
#2553=CARTESIAN_POINT('Ctrl Pts',(-1.84370531767661,13.3744430502294,6.55));
#2554=CARTESIAN_POINT('Ctrl Pts',(-1.67642144832972,13.3964062370615,6.51887197142702));
#2555=CARTESIAN_POINT('Ctrl Pts',(-1.36798879559555,13.431407059342,6.39128997486268));
#2556=CARTESIAN_POINT('Ctrl Pts',(-1.22686674457499,13.4446014654523,6.29481443961593));
#2557=CARTESIAN_POINT('Ctrl Pts',(-1.00475112921042,13.4630160869044,6.07233750789797));
#2558=CARTESIAN_POINT('Ctrl Pts',(-0.908716991768158,13.4695324913417,5.93192759707115));
#2559=CARTESIAN_POINT('Ctrl Pts',(-0.781341233035619,13.4775212102557,5.62419425457921));
#2560=CARTESIAN_POINT('Ctrl Pts',(-0.75,13.4791505667086,5.4568747590473));
#2561=CARTESIAN_POINT('Ctrl Pts',(-0.75,13.4791505667086,5.1431252409527));
#2562=CARTESIAN_POINT('Ctrl Pts',(-0.78134123303562,13.4775212102557,4.97580574542079));
#2563=CARTESIAN_POINT('Ctrl Pts',(-0.908716991768159,13.4695324913417,4.66807240292884));
#2564=CARTESIAN_POINT('Ctrl Pts',(-1.00475112921042,13.4630160869044,4.52766249210203));
#2565=CARTESIAN_POINT('Ctrl Pts',(-1.22686674457499,13.4446014654523,4.30518556038407));
#2566=CARTESIAN_POINT('Ctrl Pts',(-1.36798879559555,13.431407059342,4.20871002513732));
#2567=CARTESIAN_POINT('Ctrl Pts',(-1.67642144832971,13.3964062370615,4.08112802857298));
#2568=CARTESIAN_POINT('Ctrl Pts',(-1.84370531767661,13.3744430502294,4.05));
#2569=CARTESIAN_POINT('Ctrl Pts',(-2.15801374389282,13.3273592779611,4.05));
#2570=CARTESIAN_POINT('Ctrl Pts',(-2.32609557960331,13.2990210880236,4.08174447813834));
#2571=CARTESIAN_POINT('Ctrl Pts',(-2.6349594886099,13.2412866081987,4.21036185969659));
#2572=CARTESIAN_POINT('Ctrl Pts',(-2.77577516736032,13.2120416331141,4.30722193842639));
#2573=CARTESIAN_POINT('Ctrl Pts',(-2.99640130889512,13.163742383297,4.52942961273184));
#2574=CARTESIAN_POINT('Ctrl Pts',(-3.09176308346025,13.1413566197491,4.66905127000784));
#2575=CARTESIAN_POINT('Ctrl Pts',(-3.21857778155663,13.1108737267815,4.97579162907471));
#2576=CARTESIAN_POINT('Ctrl Pts',(-3.25,13.1029576813787,5.1429409924733));
#2577=CARTESIAN_POINT('Ctrl Pts',(-3.25,13.1029576813787,5.3));
#2578=CARTESIAN_POINT('',(-3.25,0.,5.3));
#2579=CARTESIAN_POINT('Origin',(-2.,-26.9,5.3));
#2580=CARTESIAN_POINT('',(-3.45,-27.,5.3));
#2581=CARTESIAN_POINT('Origin',(-2.,-27.,5.3));
#2582=CARTESIAN_POINT('',(-3.25,-26.8,5.3));
#2583=CARTESIAN_POINT('',(-3.35,-26.9,5.3));
#2584=CARTESIAN_POINT('Origin',(-2.,-26.8,5.3));
#2585=CARTESIAN_POINT('Origin',(-7.97967105517399,-27.,0.));
#2586=CARTESIAN_POINT('',(6.25103652921323,-27.,0.4));
#2587=CARTESIAN_POINT('',(-6.25103652921324,-27.,0.4));
#2588=CARTESIAN_POINT('',(-3.98983552758699,-27.,0.4));
#2589=CARTESIAN_POINT('',(6.25103652921323,-27.,8.2));
#2590=CARTESIAN_POINT('',(6.25103652921323,-27.,0.));
#2591=CARTESIAN_POINT('',(-6.25103652921324,-27.,8.2));
#2592=CARTESIAN_POINT('',(-3.98983552758699,-27.,8.2));
#2593=CARTESIAN_POINT('',(-6.25103652921324,-27.,0.));
#2594=CARTESIAN_POINT('',(0.55,-27.,5.3));
#2595=CARTESIAN_POINT('Origin',(2.,-27.,5.3));
#2596=CARTESIAN_POINT('Origin',(-2.,0.,5.3));
#2597=CARTESIAN_POINT('',(-3.25,-13.1029576813787,5.3));
#2598=CARTESIAN_POINT('',(-3.25,0.,5.3));
#2599=CARTESIAN_POINT('Ctrl Pts',(-3.25,-13.1029576813787,5.3));
#2600=CARTESIAN_POINT('Ctrl Pts',(-3.25,-13.1029576813787,5.1429409924733));
#2601=CARTESIAN_POINT('Ctrl Pts',(-3.21857778155663,-13.1108737267815,4.97579162907471));
#2602=CARTESIAN_POINT('Ctrl Pts',(-3.09176308346025,-13.1413566197491,4.66905127000784));
#2603=CARTESIAN_POINT('Ctrl Pts',(-2.99640130889512,-13.163742383297,4.52942961273184));
#2604=CARTESIAN_POINT('Ctrl Pts',(-2.77577516736032,-13.2120416331141,4.30722193842639));
#2605=CARTESIAN_POINT('Ctrl Pts',(-2.6349594886099,-13.2412866081987,4.21036185969658));
#2606=CARTESIAN_POINT('Ctrl Pts',(-2.32609557960331,-13.2990210880236,4.08174447813834));
#2607=CARTESIAN_POINT('Ctrl Pts',(-2.15801374389282,-13.3273592779611,4.05));
#2608=CARTESIAN_POINT('Ctrl Pts',(-1.84370531767661,-13.3744430502294,4.05));
#2609=CARTESIAN_POINT('Ctrl Pts',(-1.67642144832971,-13.3964062370615,4.08112802857298));
#2610=CARTESIAN_POINT('Ctrl Pts',(-1.36798879559555,-13.431407059342,4.20871002513732));
#2611=CARTESIAN_POINT('Ctrl Pts',(-1.22686674457499,-13.4446014654523,4.30518556038407));
#2612=CARTESIAN_POINT('Ctrl Pts',(-1.00475112921042,-13.4630160869044,4.52766249210203));
#2613=CARTESIAN_POINT('Ctrl Pts',(-0.908716991768159,-13.4695324913417,
4.66807240292884));
#2614=CARTESIAN_POINT('Ctrl Pts',(-0.78134123303562,-13.4775212102557,4.97580574542079));
#2615=CARTESIAN_POINT('Ctrl Pts',(-0.75,-13.4791505667086,5.1431252409527));
#2616=CARTESIAN_POINT('Ctrl Pts',(-0.75,-13.4791505667086,5.4568747590473));
#2617=CARTESIAN_POINT('Ctrl Pts',(-0.781341233035619,-13.4775212102557,
5.62419425457921));
#2618=CARTESIAN_POINT('Ctrl Pts',(-0.908716991768159,-13.4695324913417,
5.93192759707116));
#2619=CARTESIAN_POINT('Ctrl Pts',(-1.00475112921042,-13.4630160869044,6.07233750789797));
#2620=CARTESIAN_POINT('Ctrl Pts',(-1.22686674457499,-13.4446014654523,6.29481443961593));
#2621=CARTESIAN_POINT('Ctrl Pts',(-1.36798879559555,-13.431407059342,6.39128997486268));
#2622=CARTESIAN_POINT('Ctrl Pts',(-1.67642144832971,-13.3964062370615,6.51887197142702));
#2623=CARTESIAN_POINT('Ctrl Pts',(-1.84370531767661,-13.3744430502294,6.55));
#2624=CARTESIAN_POINT('Ctrl Pts',(-2.15801374389282,-13.3273592779611,6.55));
#2625=CARTESIAN_POINT('Ctrl Pts',(-2.32609557960331,-13.2990210880236,6.51825552186166));
#2626=CARTESIAN_POINT('Ctrl Pts',(-2.6349594886099,-13.2412866081987,6.38963814030342));
#2627=CARTESIAN_POINT('Ctrl Pts',(-2.77577516736032,-13.2120416331141,6.29277806157361));
#2628=CARTESIAN_POINT('Ctrl Pts',(-2.99640130889512,-13.163742383297,6.07057038726816));
#2629=CARTESIAN_POINT('Ctrl Pts',(-3.09176308346025,-13.1413566197491,5.93094872999216));
#2630=CARTESIAN_POINT('Ctrl Pts',(-3.21857778155664,-13.1108737267815,5.6242083709253));
#2631=CARTESIAN_POINT('Ctrl Pts',(-3.25,-13.1029576813787,5.4570590075267));
#2632=CARTESIAN_POINT('Ctrl Pts',(-3.25,-13.1029576813787,5.3));
#2633=CARTESIAN_POINT('Origin',(2.,26.9,5.3));
#2634=CARTESIAN_POINT('',(0.75,26.8,5.3));
#2635=CARTESIAN_POINT('',(0.65,26.9,5.3));
#2636=CARTESIAN_POINT('Origin',(2.,26.8,5.3));
#2637=CARTESIAN_POINT('Origin',(2.,0.,5.3));
#2638=CARTESIAN_POINT('',(0.75,13.4791505667086,5.3));
#2639=CARTESIAN_POINT('Ctrl Pts',(0.75,13.4791505667086,5.3));
#2640=CARTESIAN_POINT('Ctrl Pts',(0.75,13.4791505667086,5.4568747590473));
#2641=CARTESIAN_POINT('Ctrl Pts',(0.781341233035619,13.4775212102557,5.62419425457921));
#2642=CARTESIAN_POINT('Ctrl Pts',(0.908716991768159,13.4695324913417,5.93192759707116));
#2643=CARTESIAN_POINT('Ctrl Pts',(1.00475112921042,13.4630160869044,6.07233750789797));
#2644=CARTESIAN_POINT('Ctrl Pts',(1.22686674457499,13.4446014654523,6.29481443961593));
#2645=CARTESIAN_POINT('Ctrl Pts',(1.36798879559555,13.431407059342,6.39128997486268));
#2646=CARTESIAN_POINT('Ctrl Pts',(1.67642144832971,13.3964062370615,6.51887197142702));
#2647=CARTESIAN_POINT('Ctrl Pts',(1.84370531767661,13.3744430502294,6.55));
#2648=CARTESIAN_POINT('Ctrl Pts',(2.15801374389282,13.3273592779611,6.55));
#2649=CARTESIAN_POINT('Ctrl Pts',(2.32609557960331,13.2990210880236,6.51825552186166));
#2650=CARTESIAN_POINT('Ctrl Pts',(2.6349594886099,13.2412866081987,6.38963814030341));
#2651=CARTESIAN_POINT('Ctrl Pts',(2.77577516736032,13.2120416331141,6.29277806157361));
#2652=CARTESIAN_POINT('Ctrl Pts',(2.99640130889512,13.163742383297,6.07057038726816));
#2653=CARTESIAN_POINT('Ctrl Pts',(3.09176308346025,13.1413566197491,5.93094872999216));
#2654=CARTESIAN_POINT('Ctrl Pts',(3.21857778155664,13.1108737267815,5.6242083709253));
#2655=CARTESIAN_POINT('Ctrl Pts',(3.25,13.1029576813787,5.45705900752669));
#2656=CARTESIAN_POINT('Ctrl Pts',(3.25,13.1029576813787,5.1429409924733));
#2657=CARTESIAN_POINT('Ctrl Pts',(3.21857778155664,13.1108737267815,4.97579162907471));
#2658=CARTESIAN_POINT('Ctrl Pts',(3.09176308346025,13.1413566197491,4.66905127000784));
#2659=CARTESIAN_POINT('Ctrl Pts',(2.99640130889512,13.163742383297,4.52942961273184));
#2660=CARTESIAN_POINT('Ctrl Pts',(2.77577516736032,13.2120416331141,4.30722193842639));
#2661=CARTESIAN_POINT('Ctrl Pts',(2.6349594886099,13.2412866081987,4.21036185969658));
#2662=CARTESIAN_POINT('Ctrl Pts',(2.32609557960331,13.2990210880236,4.08174447813834));
#2663=CARTESIAN_POINT('Ctrl Pts',(2.15801374389282,13.3273592779611,4.05));
#2664=CARTESIAN_POINT('Ctrl Pts',(1.84370531767661,13.3744430502294,4.05));
#2665=CARTESIAN_POINT('Ctrl Pts',(1.67642144832972,13.3964062370615,4.08112802857298));
#2666=CARTESIAN_POINT('Ctrl Pts',(1.36798879559555,13.431407059342,4.20871002513732));
#2667=CARTESIAN_POINT('Ctrl Pts',(1.22686674457499,13.4446014654523,4.30518556038407));
#2668=CARTESIAN_POINT('Ctrl Pts',(1.00475112921042,13.4630160869044,4.52766249210203));
#2669=CARTESIAN_POINT('Ctrl Pts',(0.908716991768159,13.4695324913417,4.66807240292884));
#2670=CARTESIAN_POINT('Ctrl Pts',(0.78134123303562,13.4775212102557,4.97580574542079));
#2671=CARTESIAN_POINT('Ctrl Pts',(0.75,13.4791505667086,5.1431252409527));
#2672=CARTESIAN_POINT('Ctrl Pts',(0.75,13.4791505667086,5.3));
#2673=CARTESIAN_POINT('',(0.75,0.,5.3));
#2674=CARTESIAN_POINT('Origin',(2.,-26.9,5.3));
#2675=CARTESIAN_POINT('',(0.75,-26.8,5.3));
#2676=CARTESIAN_POINT('',(0.65,-26.9,5.3));
#2677=CARTESIAN_POINT('Origin',(2.,-26.8,5.3));
#2678=CARTESIAN_POINT('Origin',(2.,0.,5.3));
#2679=CARTESIAN_POINT('',(0.75,-13.4791505667086,5.3));
#2680=CARTESIAN_POINT('',(0.75,0.,5.3));
#2681=CARTESIAN_POINT('Ctrl Pts',(0.75,-13.4791505667086,5.3));
#2682=CARTESIAN_POINT('Ctrl Pts',(0.75,-13.4791505667086,5.1431252409527));
#2683=CARTESIAN_POINT('Ctrl Pts',(0.78134123303562,-13.4775212102557,4.97580574542079));
#2684=CARTESIAN_POINT('Ctrl Pts',(0.908716991768159,-13.4695324913417,4.66807240292884));
#2685=CARTESIAN_POINT('Ctrl Pts',(1.00475112921042,-13.4630160869044,4.52766249210203));
#2686=CARTESIAN_POINT('Ctrl Pts',(1.22686674457499,-13.4446014654523,4.30518556038407));
#2687=CARTESIAN_POINT('Ctrl Pts',(1.36798879559555,-13.431407059342,4.20871002513732));
#2688=CARTESIAN_POINT('Ctrl Pts',(1.67642144832971,-13.3964062370615,4.08112802857298));
#2689=CARTESIAN_POINT('Ctrl Pts',(1.84370531767661,-13.3744430502294,4.05));
#2690=CARTESIAN_POINT('Ctrl Pts',(2.15801374389282,-13.3273592779611,4.05));
#2691=CARTESIAN_POINT('Ctrl Pts',(2.32609557960331,-13.2990210880236,4.08174447813834));
#2692=CARTESIAN_POINT('Ctrl Pts',(2.6349594886099,-13.2412866081987,4.21036185969658));
#2693=CARTESIAN_POINT('Ctrl Pts',(2.77577516736032,-13.2120416331141,4.30722193842639));
#2694=CARTESIAN_POINT('Ctrl Pts',(2.99640130889512,-13.163742383297,4.52942961273184));
#2695=CARTESIAN_POINT('Ctrl Pts',(3.09176308346025,-13.1413566197491,4.66905127000784));
#2696=CARTESIAN_POINT('Ctrl Pts',(3.21857778155663,-13.1108737267815,4.97579162907471));
#2697=CARTESIAN_POINT('Ctrl Pts',(3.25,-13.1029576813787,5.1429409924733));
#2698=CARTESIAN_POINT('Ctrl Pts',(3.25,-13.1029576813787,5.45705900752669));
#2699=CARTESIAN_POINT('Ctrl Pts',(3.21857778155664,-13.1108737267815,5.6242083709253));
#2700=CARTESIAN_POINT('Ctrl Pts',(3.09176308346025,-13.1413566197491,5.93094872999216));
#2701=CARTESIAN_POINT('Ctrl Pts',(2.99640130889512,-13.163742383297,6.07057038726816));
#2702=CARTESIAN_POINT('Ctrl Pts',(2.77577516736032,-13.2120416331141,6.29277806157361));
#2703=CARTESIAN_POINT('Ctrl Pts',(2.6349594886099,-13.2412866081987,6.38963814030341));
#2704=CARTESIAN_POINT('Ctrl Pts',(2.32609557960331,-13.2990210880236,6.51825552186166));
#2705=CARTESIAN_POINT('Ctrl Pts',(2.15801374389282,-13.3273592779611,6.55));
#2706=CARTESIAN_POINT('Ctrl Pts',(1.84370531767661,-13.3744430502294,6.55));
#2707=CARTESIAN_POINT('Ctrl Pts',(1.67642144832971,-13.3964062370615,6.51887197142702));
#2708=CARTESIAN_POINT('Ctrl Pts',(1.36798879559555,-13.431407059342,6.39128997486268));
#2709=CARTESIAN_POINT('Ctrl Pts',(1.22686674457499,-13.4446014654523,6.29481443961593));
#2710=CARTESIAN_POINT('Ctrl Pts',(1.00475112921042,-13.4630160869044,6.07233750789797));
#2711=CARTESIAN_POINT('Ctrl Pts',(0.908716991768159,-13.4695324913417,5.93192759707116));
#2712=CARTESIAN_POINT('Ctrl Pts',(0.78134123303562,-13.4775212102557,5.62419425457921));
#2713=CARTESIAN_POINT('Ctrl Pts',(0.75,-13.4791505667086,5.4568747590473));
#2714=CARTESIAN_POINT('Ctrl Pts',(0.75,-13.4791505667086,5.3));
#2715=CARTESIAN_POINT('Origin',(0.,2.,5.3));
#2716=CARTESIAN_POINT('',(-20.2009618943233,3.25,5.3));
#2717=CARTESIAN_POINT('',(-18.627718676731,2.,6.55));
#2718=CARTESIAN_POINT('Ctrl Pts',(-20.2009618943233,3.25,5.3));
#2719=CARTESIAN_POINT('Ctrl Pts',(-20.2009618943233,3.25,5.39029234212096));
#2720=CARTESIAN_POINT('Ctrl Pts',(-20.1772005951641,3.24064153091951,5.47120219564432));
#2721=CARTESIAN_POINT('Ctrl Pts',(-20.1045047934154,3.2100076151372,5.62308391879915));
#2722=CARTESIAN_POINT('Ctrl Pts',(-20.0552828276892,3.18851767079192,5.69387466967946));
#2723=CARTESIAN_POINT('Ctrl Pts',(-19.8870287687914,3.10865620052542,5.89516586902311));
#2724=CARTESIAN_POINT('Ctrl Pts',(-19.7488255069301,3.03425420344229,6.01333284729064));
#2725=CARTESIAN_POINT('Ctrl Pts',(-19.4531336124367,2.84596078128561,6.23475573757803));
#2726=CARTESIAN_POINT('Ctrl Pts',(-19.2692763372079,2.70748360064366,6.34637446065784));
#2727=CARTESIAN_POINT('Ctrl Pts',(-18.9234249011479,2.38072616471554,6.50435864359466));
#2728=CARTESIAN_POINT('Ctrl Pts',(-18.7614575952714,2.19206789895891,6.55));
#2729=CARTESIAN_POINT('Ctrl Pts',(-18.627718676731,2.,6.55));
#2730=CARTESIAN_POINT('Ctrl Pts',(-18.627718676731,2.,6.55));
#2731=CARTESIAN_POINT('Ctrl Pts',(-18.5268891231803,1.85519457825137,6.55));
#2732=CARTESIAN_POINT('Ctrl Pts',(-18.4305104297577,1.69087323617109,6.52306381241391));
#2733=CARTESIAN_POINT('Ctrl Pts',(-18.2767214624013,1.37524312511396,6.39595782382434));
#2734=CARTESIAN_POINT('Ctrl Pts',(-18.2187291193599,1.22443201701213,6.29525819606588));
#2735=CARTESIAN_POINT('Ctrl Pts',(-18.1436817901795,0.998771663818447,6.06355058537597));
#2736=CARTESIAN_POINT('Ctrl Pts',(-18.1184989197252,0.905294021223847,5.92537474512899));
#2737=CARTESIAN_POINT('Ctrl Pts',(-18.0876253164435,0.780900542172468,5.62135879792505));
#2738=CARTESIAN_POINT('Ctrl Pts',(-18.0813014172057,0.75,5.45557706538823));
#2739=CARTESIAN_POINT('Ctrl Pts',(-18.0813014172057,0.75,5.14442293461177));
#2740=CARTESIAN_POINT('Ctrl Pts',(-18.0876253164435,0.780900542172469,4.97864120207495));
#2741=CARTESIAN_POINT('Ctrl Pts',(-18.1184989197252,0.905294021223848,4.67462525487101));
#2742=CARTESIAN_POINT('Ctrl Pts',(-18.1436817901795,0.998771663818447,4.53644941462403));
#2743=CARTESIAN_POINT('Ctrl Pts',(-18.2187291193599,1.22443201701213,4.30474180393412));
#2744=CARTESIAN_POINT('Ctrl Pts',(-18.2767214624013,1.37524312511396,4.20404217617566));
#2745=CARTESIAN_POINT('Ctrl Pts',(-18.4305104297577,1.69087323617109,4.07693618758609));
#2746=CARTESIAN_POINT('Ctrl Pts',(-18.5268891231803,1.85519457825137,4.05));
#2747=CARTESIAN_POINT('Ctrl Pts',(-18.7614575952714,2.19206789895891,4.05));
#2748=CARTESIAN_POINT('Ctrl Pts',(-18.9234249011479,2.38072616471554,4.09564135640534));
#2749=CARTESIAN_POINT('Ctrl Pts',(-19.2692763372079,2.70748360064366,4.25362553934216));
#2750=CARTESIAN_POINT('Ctrl Pts',(-19.4531336124367,2.84596078128562,4.36524426242197));
#2751=CARTESIAN_POINT('Ctrl Pts',(-19.7488255069301,3.03425420344229,4.58666715270936));
#2752=CARTESIAN_POINT('Ctrl Pts',(-19.8870287687914,3.10865620052542,4.70483413097689));
#2753=CARTESIAN_POINT('Ctrl Pts',(-20.0552828276892,3.18851767079192,4.90612533032054));
#2754=CARTESIAN_POINT('Ctrl Pts',(-20.1045047934154,3.2100076151372,4.97691608120085));
#2755=CARTESIAN_POINT('Ctrl Pts',(-20.1772005951641,3.24064153091951,5.12879780435568));
#2756=CARTESIAN_POINT('Ctrl Pts',(-20.2009618943233,3.25,5.20970765787903));
#2757=CARTESIAN_POINT('Ctrl Pts',(-20.2009618943233,3.25,5.3));
#2758=CARTESIAN_POINT('',(-13.3510299228187,2.,6.55));
#2759=CARTESIAN_POINT('',(0.,2.,6.55));
#2760=CARTESIAN_POINT('',(-13.1029576813787,3.25,5.3));
#2761=CARTESIAN_POINT('Ctrl Pts',(-13.1029576813787,3.25,5.3));
#2762=CARTESIAN_POINT('Ctrl Pts',(-13.1029576813787,3.25,5.1429409924733));
#2763=CARTESIAN_POINT('Ctrl Pts',(-13.1108737267815,3.21857778155663,4.97579162907471));
#2764=CARTESIAN_POINT('Ctrl Pts',(-13.1413566197491,3.09176308346025,4.66905127000784));
#2765=CARTESIAN_POINT('Ctrl Pts',(-13.163742383297,2.99640130889512,4.52942961273184));
#2766=CARTESIAN_POINT('Ctrl Pts',(-13.2120416331141,2.77577516736032,4.30722193842639));
#2767=CARTESIAN_POINT('Ctrl Pts',(-13.2412866081987,2.6349594886099,4.21036185969658));
#2768=CARTESIAN_POINT('Ctrl Pts',(-13.2990210880236,2.32609557960331,4.08174447813834));
#2769=CARTESIAN_POINT('Ctrl Pts',(-13.3273592779611,2.15801374389282,4.05));
#2770=CARTESIAN_POINT('Ctrl Pts',(-13.3744430502294,1.84370531767661,4.05));
#2771=CARTESIAN_POINT('Ctrl Pts',(-13.3964062370615,1.67642144832971,4.08112802857298));
#2772=CARTESIAN_POINT('Ctrl Pts',(-13.431407059342,1.36798879559555,4.20871002513732));
#2773=CARTESIAN_POINT('Ctrl Pts',(-13.4446014654523,1.22686674457499,4.30518556038407));
#2774=CARTESIAN_POINT('Ctrl Pts',(-13.4630160869044,1.00475112921042,4.52766249210203));
#2775=CARTESIAN_POINT('Ctrl Pts',(-13.4695324913417,0.908716991768159,4.66807240292884));
#2776=CARTESIAN_POINT('Ctrl Pts',(-13.4775212102557,0.78134123303562,4.97580574542079));
#2777=CARTESIAN_POINT('Ctrl Pts',(-13.4791505667086,0.75,5.1431252409527));
#2778=CARTESIAN_POINT('Ctrl Pts',(-13.4791505667086,0.75,5.4568747590473));
#2779=CARTESIAN_POINT('Ctrl Pts',(-13.4775212102557,0.781341233035619,5.62419425457921));
#2780=CARTESIAN_POINT('Ctrl Pts',(-13.4695324913417,0.908716991768159,5.93192759707116));
#2781=CARTESIAN_POINT('Ctrl Pts',(-13.4630160869044,1.00475112921042,6.07233750789797));
#2782=CARTESIAN_POINT('Ctrl Pts',(-13.4446014654523,1.22686674457499,6.29481443961593));
#2783=CARTESIAN_POINT('Ctrl Pts',(-13.431407059342,1.36798879559555,6.39128997486268));
#2784=CARTESIAN_POINT('Ctrl Pts',(-13.3964062370615,1.67642144832971,6.51887197142702));
#2785=CARTESIAN_POINT('Ctrl Pts',(-13.3744430502294,1.84370531767661,6.55));
#2786=CARTESIAN_POINT('Ctrl Pts',(-13.3510299228187,2.,6.55));
#2787=CARTESIAN_POINT('Ctrl Pts',(-13.3510299228187,2.,6.55));
#2788=CARTESIAN_POINT('Ctrl Pts',(-13.3273592779611,2.15801374389282,6.55));
#2789=CARTESIAN_POINT('Ctrl Pts',(-13.2990210880236,2.32609557960331,6.51825552186166));
#2790=CARTESIAN_POINT('Ctrl Pts',(-13.2412866081987,2.6349594886099,6.38963814030342));
#2791=CARTESIAN_POINT('Ctrl Pts',(-13.2120416331141,2.77577516736032,6.29277806157361));
#2792=CARTESIAN_POINT('Ctrl Pts',(-13.163742383297,2.99640130889512,6.07057038726816));
#2793=CARTESIAN_POINT('Ctrl Pts',(-13.1413566197491,3.09176308346025,5.93094872999216));
#2794=CARTESIAN_POINT('Ctrl Pts',(-13.1108737267815,3.21857778155664,5.6242083709253));
#2795=CARTESIAN_POINT('Ctrl Pts',(-13.1029576813787,3.25,5.4570590075267));
#2796=CARTESIAN_POINT('Ctrl Pts',(-13.1029576813787,3.25,5.3));
#2797=CARTESIAN_POINT('Origin',(0.,2.,5.3));
#2798=CARTESIAN_POINT('',(13.1029576813787,3.25,5.3));
#2799=CARTESIAN_POINT('',(13.3510299228187,2.,6.55));
#2800=CARTESIAN_POINT('Ctrl Pts',(13.1029576813787,3.25,5.3));
#2801=CARTESIAN_POINT('Ctrl Pts',(13.1029576813787,3.25,5.45705900752669));
#2802=CARTESIAN_POINT('Ctrl Pts',(13.1108737267815,3.21857778155664,5.6242083709253));
#2803=CARTESIAN_POINT('Ctrl Pts',(13.1413566197491,3.09176308346025,5.93094872999216));
#2804=CARTESIAN_POINT('Ctrl Pts',(13.163742383297,2.99640130889512,6.07057038726816));
#2805=CARTESIAN_POINT('Ctrl Pts',(13.2120416331141,2.77577516736032,6.29277806157361));
#2806=CARTESIAN_POINT('Ctrl Pts',(13.2412866081987,2.6349594886099,6.38963814030342));
#2807=CARTESIAN_POINT('Ctrl Pts',(13.2990210880236,2.32609557960331,6.51825552186166));
#2808=CARTESIAN_POINT('Ctrl Pts',(13.3273592779611,2.15801374389282,6.55));
#2809=CARTESIAN_POINT('Ctrl Pts',(13.3510299228187,2.,6.55));
#2810=CARTESIAN_POINT('Ctrl Pts',(13.3510299228187,2.,6.55));
#2811=CARTESIAN_POINT('Ctrl Pts',(13.3744430502294,1.84370531767661,6.55));
#2812=CARTESIAN_POINT('Ctrl Pts',(13.3964062370615,1.67642144832971,6.51887197142702));
#2813=CARTESIAN_POINT('Ctrl Pts',(13.431407059342,1.36798879559555,6.39128997486268));
#2814=CARTESIAN_POINT('Ctrl Pts',(13.4446014654523,1.22686674457499,6.29481443961593));
#2815=CARTESIAN_POINT('Ctrl Pts',(13.4630160869044,1.00475112921042,6.07233750789797));
#2816=CARTESIAN_POINT('Ctrl Pts',(13.4695324913417,0.908716991768159,5.93192759707116));
#2817=CARTESIAN_POINT('Ctrl Pts',(13.4775212102557,0.781341233035619,5.62419425457921));
#2818=CARTESIAN_POINT('Ctrl Pts',(13.4791505667086,0.75,5.4568747590473));
#2819=CARTESIAN_POINT('Ctrl Pts',(13.4791505667086,0.75,5.1431252409527));
#2820=CARTESIAN_POINT('Ctrl Pts',(13.4775212102557,0.78134123303562,4.97580574542079));
#2821=CARTESIAN_POINT('Ctrl Pts',(13.4695324913417,0.908716991768159,4.66807240292884));
#2822=CARTESIAN_POINT('Ctrl Pts',(13.4630160869044,1.00475112921042,4.52766249210203));
#2823=CARTESIAN_POINT('Ctrl Pts',(13.4446014654523,1.22686674457499,4.30518556038407));
#2824=CARTESIAN_POINT('Ctrl Pts',(13.431407059342,1.36798879559555,4.20871002513732));
#2825=CARTESIAN_POINT('Ctrl Pts',(13.3964062370615,1.67642144832971,4.08112802857298));
#2826=CARTESIAN_POINT('Ctrl Pts',(13.3744430502294,1.84370531767661,4.05));
#2827=CARTESIAN_POINT('Ctrl Pts',(13.3273592779611,2.15801374389282,4.05));
#2828=CARTESIAN_POINT('Ctrl Pts',(13.2990210880236,2.32609557960331,4.08174447813834));
#2829=CARTESIAN_POINT('Ctrl Pts',(13.2412866081987,2.6349594886099,4.21036185969658));
#2830=CARTESIAN_POINT('Ctrl Pts',(13.2120416331141,2.77577516736032,4.30722193842639));
#2831=CARTESIAN_POINT('Ctrl Pts',(13.163742383297,2.99640130889512,4.52942961273184));
#2832=CARTESIAN_POINT('Ctrl Pts',(13.1413566197491,3.09176308346025,4.66905127000784));
#2833=CARTESIAN_POINT('Ctrl Pts',(13.1108737267815,3.21857778155663,4.97579162907471));
#2834=CARTESIAN_POINT('Ctrl Pts',(13.1029576813787,3.25,5.1429409924733));
#2835=CARTESIAN_POINT('Ctrl Pts',(13.1029576813787,3.25,5.3));
#2836=CARTESIAN_POINT('',(18.627718676731,2.,6.55));
#2837=CARTESIAN_POINT('',(0.,2.,6.55));
#2838=CARTESIAN_POINT('',(20.2009618943233,3.25,5.3));
#2839=CARTESIAN_POINT('Ctrl Pts',(20.2009618943233,3.25,5.3));
#2840=CARTESIAN_POINT('Ctrl Pts',(20.2009618943233,3.25,5.20970765787903));
#2841=CARTESIAN_POINT('Ctrl Pts',(20.1772005951641,3.24064153091951,5.12879780435568));
#2842=CARTESIAN_POINT('Ctrl Pts',(20.1045047934154,3.2100076151372,4.97691608120085));
#2843=CARTESIAN_POINT('Ctrl Pts',(20.0552828276892,3.18851767079192,4.90612533032054));
#2844=CARTESIAN_POINT('Ctrl Pts',(19.8870287687914,3.10865620052542,4.70483413097689));
#2845=CARTESIAN_POINT('Ctrl Pts',(19.7488255069301,3.03425420344229,4.58666715270936));
#2846=CARTESIAN_POINT('Ctrl Pts',(19.4531336124367,2.84596078128561,4.36524426242197));
#2847=CARTESIAN_POINT('Ctrl Pts',(19.2692763372079,2.70748360064366,4.25362553934216));
#2848=CARTESIAN_POINT('Ctrl Pts',(18.9234249011479,2.38072616471554,4.09564135640534));
#2849=CARTESIAN_POINT('Ctrl Pts',(18.7614575952714,2.19206789895891,4.05));
#2850=CARTESIAN_POINT('Ctrl Pts',(18.5268891231803,1.85519457825137,4.05));
#2851=CARTESIAN_POINT('Ctrl Pts',(18.4305104297577,1.69087323617109,4.07693618758609));
#2852=CARTESIAN_POINT('Ctrl Pts',(18.2767214624013,1.37524312511396,4.20404217617566));
#2853=CARTESIAN_POINT('Ctrl Pts',(18.2187291193599,1.22443201701213,4.30474180393412));
#2854=CARTESIAN_POINT('Ctrl Pts',(18.1436817901795,0.998771663818447,4.53644941462403));
#2855=CARTESIAN_POINT('Ctrl Pts',(18.1184989197252,0.905294021223847,4.67462525487101));
#2856=CARTESIAN_POINT('Ctrl Pts',(18.0876253164435,0.780900542172469,4.97864120207495));
#2857=CARTESIAN_POINT('Ctrl Pts',(18.0813014172057,0.75,5.14442293461177));
#2858=CARTESIAN_POINT('Ctrl Pts',(18.0813014172057,0.75,5.45557706538823));
#2859=CARTESIAN_POINT('Ctrl Pts',(18.0876253164435,0.780900542172469,5.62135879792505));
#2860=CARTESIAN_POINT('Ctrl Pts',(18.1184989197252,0.905294021223848,5.92537474512899));
#2861=CARTESIAN_POINT('Ctrl Pts',(18.1436817901795,0.998771663818447,6.06355058537597));
#2862=CARTESIAN_POINT('Ctrl Pts',(18.2187291193599,1.22443201701213,6.29525819606588));
#2863=CARTESIAN_POINT('Ctrl Pts',(18.2767214624013,1.37524312511396,6.39595782382434));
#2864=CARTESIAN_POINT('Ctrl Pts',(18.4305104297577,1.69087323617109,6.52306381241391));
#2865=CARTESIAN_POINT('Ctrl Pts',(18.5268891231803,1.85519457825137,6.55));
#2866=CARTESIAN_POINT('Ctrl Pts',(18.627718676731,2.,6.55));
#2867=CARTESIAN_POINT('Ctrl Pts',(18.627718676731,2.,6.55));
#2868=CARTESIAN_POINT('Ctrl Pts',(18.7614575952714,2.19206789895891,6.55));
#2869=CARTESIAN_POINT('Ctrl Pts',(18.9234249011479,2.38072616471554,6.50435864359466));
#2870=CARTESIAN_POINT('Ctrl Pts',(19.2692763372079,2.70748360064366,6.34637446065784));
#2871=CARTESIAN_POINT('Ctrl Pts',(19.4531336124367,2.84596078128561,6.23475573757803));
#2872=CARTESIAN_POINT('Ctrl Pts',(19.7488255069301,3.03425420344229,6.01333284729064));
#2873=CARTESIAN_POINT('Ctrl Pts',(19.8870287687914,3.10865620052542,5.89516586902311));
#2874=CARTESIAN_POINT('Ctrl Pts',(20.0552828276892,3.18851767079192,5.69387466967946));
#2875=CARTESIAN_POINT('Ctrl Pts',(20.1045047934154,3.2100076151372,5.62308391879915));
#2876=CARTESIAN_POINT('Ctrl Pts',(20.1772005951641,3.24064153091951,5.47120219564432));
#2877=CARTESIAN_POINT('Ctrl Pts',(20.2009618943233,3.25,5.39029234212096));
#2878=CARTESIAN_POINT('Ctrl Pts',(20.2009618943233,3.25,5.3));
#2879=CARTESIAN_POINT('Origin',(0.,-2.,5.3));
#2880=CARTESIAN_POINT('',(-18.0813014172057,-0.75,5.3));
#2881=CARTESIAN_POINT('',(-18.627718676731,-2.,6.55));
#2882=CARTESIAN_POINT('Ctrl Pts',(-18.0813014172057,-0.75,5.3));
#2883=CARTESIAN_POINT('Ctrl Pts',(-18.0813014172057,-0.75,5.45557706538823));
#2884=CARTESIAN_POINT('Ctrl Pts',(-18.0876253164435,-0.780900542172469,
5.62135879792505));
#2885=CARTESIAN_POINT('Ctrl Pts',(-18.1184989197252,-0.905294021223848,
5.92537474512899));
#2886=CARTESIAN_POINT('Ctrl Pts',(-18.1436817901795,-0.998771663818447,
6.06355058537597));
#2887=CARTESIAN_POINT('Ctrl Pts',(-18.2187291193599,-1.22443201701213,6.29525819606588));
#2888=CARTESIAN_POINT('Ctrl Pts',(-18.2767214624013,-1.37524312511396,6.39595782382434));
#2889=CARTESIAN_POINT('Ctrl Pts',(-18.4305104297577,-1.69087323617109,6.52306381241391));
#2890=CARTESIAN_POINT('Ctrl Pts',(-18.5268891231803,-1.85519457825137,6.55));
#2891=CARTESIAN_POINT('Ctrl Pts',(-18.627718676731,-2.,6.55));
#2892=CARTESIAN_POINT('Ctrl Pts',(-18.627718676731,-2.,6.55));
#2893=CARTESIAN_POINT('Ctrl Pts',(-18.7614575952714,-2.19206789895891,6.55));
#2894=CARTESIAN_POINT('Ctrl Pts',(-18.9234249011479,-2.38072616471554,6.50435864359466));
#2895=CARTESIAN_POINT('Ctrl Pts',(-19.2692763372079,-2.70748360064366,6.34637446065784));
#2896=CARTESIAN_POINT('Ctrl Pts',(-19.4531336124367,-2.84596078128561,6.23475573757803));
#2897=CARTESIAN_POINT('Ctrl Pts',(-19.7488255069301,-3.03425420344229,6.01333284729064));
#2898=CARTESIAN_POINT('Ctrl Pts',(-19.8870287687914,-3.10865620052542,5.89516586902311));
#2899=CARTESIAN_POINT('Ctrl Pts',(-20.0552828276892,-3.18851767079192,5.69387466967946));
#2900=CARTESIAN_POINT('Ctrl Pts',(-20.1045047934154,-3.2100076151372,5.62308391879915));
#2901=CARTESIAN_POINT('Ctrl Pts',(-20.1772005951641,-3.24064153091951,5.47120219564432));
#2902=CARTESIAN_POINT('Ctrl Pts',(-20.2009618943233,-3.25,5.39029234212096));
#2903=CARTESIAN_POINT('Ctrl Pts',(-20.2009618943233,-3.25,5.20970765787903));
#2904=CARTESIAN_POINT('Ctrl Pts',(-20.1772005951641,-3.24064153091951,5.12879780435568));
#2905=CARTESIAN_POINT('Ctrl Pts',(-20.1045047934154,-3.2100076151372,4.97691608120085));
#2906=CARTESIAN_POINT('Ctrl Pts',(-20.0552828276892,-3.18851767079192,4.90612533032054));
#2907=CARTESIAN_POINT('Ctrl Pts',(-19.8870287687914,-3.10865620052542,4.70483413097689));
#2908=CARTESIAN_POINT('Ctrl Pts',(-19.7488255069301,-3.03425420344229,4.58666715270936));
#2909=CARTESIAN_POINT('Ctrl Pts',(-19.4531336124367,-2.84596078128561,4.36524426242197));
#2910=CARTESIAN_POINT('Ctrl Pts',(-19.2692763372079,-2.70748360064366,4.25362553934216));
#2911=CARTESIAN_POINT('Ctrl Pts',(-18.9234249011479,-2.38072616471554,4.09564135640534));
#2912=CARTESIAN_POINT('Ctrl Pts',(-18.7614575952714,-2.19206789895891,4.05));
#2913=CARTESIAN_POINT('Ctrl Pts',(-18.5268891231803,-1.85519457825137,4.05));
#2914=CARTESIAN_POINT('Ctrl Pts',(-18.4305104297577,-1.69087323617109,4.0769361875861));
#2915=CARTESIAN_POINT('Ctrl Pts',(-18.2767214624013,-1.37524312511396,4.20404217617566));
#2916=CARTESIAN_POINT('Ctrl Pts',(-18.2187291193599,-1.22443201701213,4.30474180393412));
#2917=CARTESIAN_POINT('Ctrl Pts',(-18.1436817901795,-0.998771663818447,
4.53644941462403));
#2918=CARTESIAN_POINT('Ctrl Pts',(-18.1184989197252,-0.905294021223848,
4.67462525487101));
#2919=CARTESIAN_POINT('Ctrl Pts',(-18.0876253164435,-0.780900542172469,
4.97864120207495));
#2920=CARTESIAN_POINT('Ctrl Pts',(-18.0813014172057,-0.75,5.14442293461177));
#2921=CARTESIAN_POINT('Ctrl Pts',(-18.0813014172057,-0.75,5.3));
#2922=CARTESIAN_POINT('',(-13.3510299228187,-2.,6.55));
#2923=CARTESIAN_POINT('',(0.,-2.,6.55));
#2924=CARTESIAN_POINT('',(-13.4791505667086,-0.75,5.3));
#2925=CARTESIAN_POINT('Ctrl Pts',(-13.4791505667086,-0.75,5.3));
#2926=CARTESIAN_POINT('Ctrl Pts',(-13.4791505667086,-0.75,5.1431252409527));
#2927=CARTESIAN_POINT('Ctrl Pts',(-13.4775212102557,-0.78134123303562,4.97580574542079));
#2928=CARTESIAN_POINT('Ctrl Pts',(-13.4695324913417,-0.908716991768159,
4.66807240292884));
#2929=CARTESIAN_POINT('Ctrl Pts',(-13.4630160869044,-1.00475112921042,4.52766249210203));
#2930=CARTESIAN_POINT('Ctrl Pts',(-13.4446014654523,-1.22686674457499,4.30518556038407));
#2931=CARTESIAN_POINT('Ctrl Pts',(-13.431407059342,-1.36798879559555,4.20871002513732));
#2932=CARTESIAN_POINT('Ctrl Pts',(-13.3964062370615,-1.67642144832972,4.08112802857298));
#2933=CARTESIAN_POINT('Ctrl Pts',(-13.3744430502294,-1.84370531767661,4.05));
#2934=CARTESIAN_POINT('Ctrl Pts',(-13.3273592779611,-2.15801374389282,4.05));
#2935=CARTESIAN_POINT('Ctrl Pts',(-13.2990210880236,-2.32609557960331,4.08174447813834));
#2936=CARTESIAN_POINT('Ctrl Pts',(-13.2412866081987,-2.6349594886099,4.21036185969658));
#2937=CARTESIAN_POINT('Ctrl Pts',(-13.2120416331141,-2.77577516736032,4.30722193842639));
#2938=CARTESIAN_POINT('Ctrl Pts',(-13.163742383297,-2.99640130889512,4.52942961273184));
#2939=CARTESIAN_POINT('Ctrl Pts',(-13.1413566197491,-3.09176308346025,4.66905127000784));
#2940=CARTESIAN_POINT('Ctrl Pts',(-13.1108737267815,-3.21857778155663,4.97579162907471));
#2941=CARTESIAN_POINT('Ctrl Pts',(-13.1029576813787,-3.25,5.1429409924733));
#2942=CARTESIAN_POINT('Ctrl Pts',(-13.1029576813787,-3.25,5.45705900752669));
#2943=CARTESIAN_POINT('Ctrl Pts',(-13.1108737267815,-3.21857778155664,5.6242083709253));
#2944=CARTESIAN_POINT('Ctrl Pts',(-13.1413566197491,-3.09176308346025,5.93094872999216));
#2945=CARTESIAN_POINT('Ctrl Pts',(-13.163742383297,-2.99640130889512,6.07057038726816));
#2946=CARTESIAN_POINT('Ctrl Pts',(-13.2120416331141,-2.77577516736032,6.29277806157361));
#2947=CARTESIAN_POINT('Ctrl Pts',(-13.2412866081987,-2.6349594886099,6.38963814030341));
#2948=CARTESIAN_POINT('Ctrl Pts',(-13.2990210880236,-2.32609557960331,6.51825552186166));
#2949=CARTESIAN_POINT('Ctrl Pts',(-13.3273592779611,-2.15801374389282,6.55));
#2950=CARTESIAN_POINT('Ctrl Pts',(-13.3510299228187,-2.,6.55));
#2951=CARTESIAN_POINT('Ctrl Pts',(-13.3510299228187,-2.,6.55));
#2952=CARTESIAN_POINT('Ctrl Pts',(-13.3744430502294,-1.84370531767661,6.55));
#2953=CARTESIAN_POINT('Ctrl Pts',(-13.3964062370615,-1.67642144832971,6.51887197142702));
#2954=CARTESIAN_POINT('Ctrl Pts',(-13.431407059342,-1.36798879559555,6.39128997486268));
#2955=CARTESIAN_POINT('Ctrl Pts',(-13.4446014654523,-1.22686674457499,6.29481443961593));
#2956=CARTESIAN_POINT('Ctrl Pts',(-13.4630160869044,-1.00475112921042,6.07233750789797));
#2957=CARTESIAN_POINT('Ctrl Pts',(-13.4695324913417,-0.908716991768159,
5.93192759707116));
#2958=CARTESIAN_POINT('Ctrl Pts',(-13.4775212102557,-0.781341233035619,
5.62419425457921));
#2959=CARTESIAN_POINT('Ctrl Pts',(-13.4791505667086,-0.75,5.4568747590473));
#2960=CARTESIAN_POINT('Ctrl Pts',(-13.4791505667086,-0.75,5.3));
#2961=CARTESIAN_POINT('Origin',(0.,-2.,5.3));
#2962=CARTESIAN_POINT('',(13.4791505667086,-0.75,5.3));
#2963=CARTESIAN_POINT('',(13.3510299228187,-2.,6.55));
#2964=CARTESIAN_POINT('Ctrl Pts',(13.4791505667086,-0.75,5.3));
#2965=CARTESIAN_POINT('Ctrl Pts',(13.4791505667086,-0.75,5.4568747590473));
#2966=CARTESIAN_POINT('Ctrl Pts',(13.4775212102557,-0.781341233035619,5.62419425457921));
#2967=CARTESIAN_POINT('Ctrl Pts',(13.4695324913417,-0.908716991768159,5.93192759707116));
#2968=CARTESIAN_POINT('Ctrl Pts',(13.4630160869044,-1.00475112921042,6.07233750789797));
#2969=CARTESIAN_POINT('Ctrl Pts',(13.4446014654523,-1.22686674457499,6.29481443961593));
#2970=CARTESIAN_POINT('Ctrl Pts',(13.431407059342,-1.36798879559555,6.39128997486268));
#2971=CARTESIAN_POINT('Ctrl Pts',(13.3964062370615,-1.67642144832971,6.51887197142702));
#2972=CARTESIAN_POINT('Ctrl Pts',(13.3744430502294,-1.84370531767661,6.55));
#2973=CARTESIAN_POINT('Ctrl Pts',(13.3510299228187,-2.,6.55));
#2974=CARTESIAN_POINT('Ctrl Pts',(13.3510299228187,-2.,6.55));
#2975=CARTESIAN_POINT('Ctrl Pts',(13.3273592779611,-2.15801374389282,6.55));
#2976=CARTESIAN_POINT('Ctrl Pts',(13.2990210880236,-2.32609557960331,6.51825552186166));
#2977=CARTESIAN_POINT('Ctrl Pts',(13.2412866081987,-2.6349594886099,6.38963814030341));
#2978=CARTESIAN_POINT('Ctrl Pts',(13.2120416331141,-2.77577516736032,6.29277806157361));
#2979=CARTESIAN_POINT('Ctrl Pts',(13.163742383297,-2.99640130889512,6.07057038726816));
#2980=CARTESIAN_POINT('Ctrl Pts',(13.1413566197491,-3.09176308346025,5.93094872999216));
#2981=CARTESIAN_POINT('Ctrl Pts',(13.1108737267815,-3.21857778155664,5.6242083709253));
#2982=CARTESIAN_POINT('Ctrl Pts',(13.1029576813787,-3.25,5.45705900752669));
#2983=CARTESIAN_POINT('Ctrl Pts',(13.1029576813787,-3.25,5.1429409924733));
#2984=CARTESIAN_POINT('Ctrl Pts',(13.1108737267815,-3.21857778155663,4.97579162907471));
#2985=CARTESIAN_POINT('Ctrl Pts',(13.1413566197491,-3.09176308346025,4.66905127000784));
#2986=CARTESIAN_POINT('Ctrl Pts',(13.163742383297,-2.99640130889512,4.52942961273184));
#2987=CARTESIAN_POINT('Ctrl Pts',(13.2120416331141,-2.77577516736032,4.30722193842639));
#2988=CARTESIAN_POINT('Ctrl Pts',(13.2412866081987,-2.6349594886099,4.21036185969659));
#2989=CARTESIAN_POINT('Ctrl Pts',(13.2990210880236,-2.32609557960331,4.08174447813834));
#2990=CARTESIAN_POINT('Ctrl Pts',(13.3273592779611,-2.15801374389282,4.05));
#2991=CARTESIAN_POINT('Ctrl Pts',(13.3744430502294,-1.84370531767661,4.05));
#2992=CARTESIAN_POINT('Ctrl Pts',(13.3964062370615,-1.67642144832971,4.08112802857298));
#2993=CARTESIAN_POINT('Ctrl Pts',(13.431407059342,-1.36798879559555,4.20871002513732));
#2994=CARTESIAN_POINT('Ctrl Pts',(13.4446014654523,-1.22686674457499,4.30518556038407));
#2995=CARTESIAN_POINT('Ctrl Pts',(13.4630160869044,-1.00475112921042,4.52766249210203));
#2996=CARTESIAN_POINT('Ctrl Pts',(13.4695324913417,-0.908716991768158,4.66807240292885));
#2997=CARTESIAN_POINT('Ctrl Pts',(13.4775212102557,-0.781341233035619,4.97580574542079));
#2998=CARTESIAN_POINT('Ctrl Pts',(13.4791505667086,-0.75,5.1431252409527));
#2999=CARTESIAN_POINT('Ctrl Pts',(13.4791505667086,-0.75,5.3));
#3000=CARTESIAN_POINT('',(18.627718676731,-2.,6.55));
#3001=CARTESIAN_POINT('',(0.,-2.,6.55));
#3002=CARTESIAN_POINT('',(18.0813014172057,-0.75,5.3));
#3003=CARTESIAN_POINT('Ctrl Pts',(18.0813014172057,-0.75,5.3));
#3004=CARTESIAN_POINT('Ctrl Pts',(18.0813014172057,-0.75,5.14442293461177));
#3005=CARTESIAN_POINT('Ctrl Pts',(18.0876253164435,-0.780900542172469,4.97864120207495));
#3006=CARTESIAN_POINT('Ctrl Pts',(18.1184989197252,-0.905294021223848,4.67462525487101));
#3007=CARTESIAN_POINT('Ctrl Pts',(18.1436817901795,-0.998771663818447,4.53644941462403));
#3008=CARTESIAN_POINT('Ctrl Pts',(18.2187291193599,-1.22443201701213,4.30474180393412));
#3009=CARTESIAN_POINT('Ctrl Pts',(18.2767214624013,-1.37524312511396,4.20404217617566));
#3010=CARTESIAN_POINT('Ctrl Pts',(18.4305104297577,-1.69087323617109,4.07693618758609));
#3011=CARTESIAN_POINT('Ctrl Pts',(18.5268891231803,-1.85519457825137,4.05));
#3012=CARTESIAN_POINT('Ctrl Pts',(18.7614575952714,-2.19206789895891,4.05));
#3013=CARTESIAN_POINT('Ctrl Pts',(18.9234249011479,-2.38072616471554,4.09564135640534));
#3014=CARTESIAN_POINT('Ctrl Pts',(19.2692763372079,-2.70748360064366,4.25362553934216));
#3015=CARTESIAN_POINT('Ctrl Pts',(19.4531336124367,-2.84596078128561,4.36524426242197));
#3016=CARTESIAN_POINT('Ctrl Pts',(19.7488255069301,-3.03425420344229,4.58666715270936));
#3017=CARTESIAN_POINT('Ctrl Pts',(19.8870287687914,-3.10865620052542,4.70483413097689));
#3018=CARTESIAN_POINT('Ctrl Pts',(20.0552828276892,-3.18851767079192,4.90612533032054));
#3019=CARTESIAN_POINT('Ctrl Pts',(20.1045047934154,-3.2100076151372,4.97691608120085));
#3020=CARTESIAN_POINT('Ctrl Pts',(20.1772005951641,-3.24064153091951,5.12879780435568));
#3021=CARTESIAN_POINT('Ctrl Pts',(20.2009618943233,-3.25,5.20970765787903));
#3022=CARTESIAN_POINT('Ctrl Pts',(20.2009618943233,-3.25,5.39029234212096));
#3023=CARTESIAN_POINT('Ctrl Pts',(20.1772005951641,-3.24064153091951,5.47120219564432));
#3024=CARTESIAN_POINT('Ctrl Pts',(20.1045047934154,-3.2100076151372,5.62308391879915));
#3025=CARTESIAN_POINT('Ctrl Pts',(20.0552828276892,-3.18851767079192,5.69387466967946));
#3026=CARTESIAN_POINT('Ctrl Pts',(19.8870287687914,-3.10865620052542,5.89516586902311));
#3027=CARTESIAN_POINT('Ctrl Pts',(19.7488255069301,-3.03425420344229,6.01333284729064));
#3028=CARTESIAN_POINT('Ctrl Pts',(19.4531336124367,-2.84596078128561,6.23475573757803));
#3029=CARTESIAN_POINT('Ctrl Pts',(19.2692763372079,-2.70748360064366,6.34637446065784));
#3030=CARTESIAN_POINT('Ctrl Pts',(18.9234249011479,-2.38072616471554,6.50435864359466));
#3031=CARTESIAN_POINT('Ctrl Pts',(18.7614575952714,-2.19206789895891,6.55));
#3032=CARTESIAN_POINT('Ctrl Pts',(18.627718676731,-2.,6.55));
#3033=CARTESIAN_POINT('Ctrl Pts',(18.627718676731,-2.,6.55));
#3034=CARTESIAN_POINT('Ctrl Pts',(18.5268891231803,-1.85519457825137,6.55));
#3035=CARTESIAN_POINT('Ctrl Pts',(18.4305104297577,-1.69087323617109,6.52306381241391));
#3036=CARTESIAN_POINT('Ctrl Pts',(18.2767214624013,-1.37524312511396,6.39595782382434));
#3037=CARTESIAN_POINT('Ctrl Pts',(18.2187291193599,-1.22443201701213,6.29525819606588));
#3038=CARTESIAN_POINT('Ctrl Pts',(18.1436817901795,-0.998771663818447,6.06355058537597));
#3039=CARTESIAN_POINT('Ctrl Pts',(18.1184989197252,-0.905294021223848,5.92537474512899));
#3040=CARTESIAN_POINT('Ctrl Pts',(18.0876253164435,-0.780900542172469,5.62135879792505));
#3041=CARTESIAN_POINT('Ctrl Pts',(18.0813014172057,-0.75,5.45557706538823));
#3042=CARTESIAN_POINT('Ctrl Pts',(18.0813014172057,-0.75,5.3));
#3043=CARTESIAN_POINT('Origin',(21.5,0.,3.7));
#3044=CARTESIAN_POINT('',(21.5,-3.5,3.7));
#3045=CARTESIAN_POINT('Origin',(21.5,0.,3.7));
#3046=CARTESIAN_POINT('',(21.5,-3.5,9.));
#3047=CARTESIAN_POINT('',(21.5,-3.5,3.7));
#3048=CARTESIAN_POINT('Origin',(21.5,0.,9.));
#3049=CARTESIAN_POINT('Origin',(21.5,0.,3.7));
#3050=CARTESIAN_POINT('Origin',(-21.5,0.,3.7));
#3051=CARTESIAN_POINT('',(-21.5,-3.5,3.7));
#3052=CARTESIAN_POINT('Origin',(-21.5,0.,3.7));
#3053=CARTESIAN_POINT('',(-21.5,-3.5,9.));
#3054=CARTESIAN_POINT('',(-21.5,-3.5,3.7));
#3055=CARTESIAN_POINT('Origin',(-21.5,0.,9.));
#3056=CARTESIAN_POINT('Origin',(-21.5,0.,3.7));
#3057=CARTESIAN_POINT('Origin',(0.,20.3,6.9));
#3058=CARTESIAN_POINT('',(-5.025,20.3,6.9));
#3059=CARTESIAN_POINT('Origin',(0.,20.3,6.9));
#3060=CARTESIAN_POINT('',(-5.025,20.3,9.));
#3061=CARTESIAN_POINT('',(-5.025,20.3,6.9));
#3062=CARTESIAN_POINT('Origin',(0.,20.3,9.));
#3063=CARTESIAN_POINT('Origin',(0.,20.3,6.9));
#3064=CARTESIAN_POINT('Origin',(0.,-20.3,6.9));
#3065=CARTESIAN_POINT('',(-5.025,-20.3,6.9));
#3066=CARTESIAN_POINT('Origin',(0.,-20.3,6.9));
#3067=CARTESIAN_POINT('',(-5.025,-20.3,9.));
#3068=CARTESIAN_POINT('',(-5.025,-20.3,6.9));
#3069=CARTESIAN_POINT('Origin',(0.,-20.3,9.));
#3070=CARTESIAN_POINT('Origin',(0.,-20.3,6.9));
#3071=CARTESIAN_POINT('Origin',(-3.98983552758699,-26.8,0.2));
#3072=CARTESIAN_POINT('',(6.25103652921323,-26.6,0.));
#3073=CARTESIAN_POINT('',(6.25103652921323,-26.6,0.));
#3074=CARTESIAN_POINT('',(-6.25103652921324,-26.6,0.));
#3075=CARTESIAN_POINT('',(-6.25103652921324,-27.,0.4));
#3076=CARTESIAN_POINT('',(-3.98983552758699,-26.6,0.));
#3077=CARTESIAN_POINT('Origin',(6.25103652921323,-25.,0.2));
#3078=CARTESIAN_POINT('',(7.8242989887542,-25.2912820512821,0.));
#3079=CARTESIAN_POINT('',(8.21761460363944,-25.3641025641026,0.4));
#3080=CARTESIAN_POINT('',(7.8242989887542,-25.2912820512821,0.));
#3081=CARTESIAN_POINT('Origin',(6.25103652921323,-25.,0.4));
#3082=CARTESIAN_POINT('Origin',(6.25103652921323,-25.,0.));
#3083=CARTESIAN_POINT('Origin',(29.26,-29.26,0.2));
#3084=CARTESIAN_POINT('',(25.2912820512821,-7.82429898875421,0.));
#3085=CARTESIAN_POINT('Origin',(29.26,-29.26,0.));
#3086=CARTESIAN_POINT('',(25.3641025641026,-8.21761460363945,0.4));
#3087=CARTESIAN_POINT('',(25.2912820512821,-7.82429898875421,0.));
#3088=CARTESIAN_POINT('Origin',(29.26,-29.26,0.4));
#3089=CARTESIAN_POINT('Origin',(25.,-6.25103652921323,0.2));
#3090=CARTESIAN_POINT('',(26.6,-6.25103652921323,0.));
#3091=CARTESIAN_POINT('',(26.6,-6.25103652921323,0.));
#3092=CARTESIAN_POINT('Origin',(25.,-6.25103652921323,0.4));
#3093=CARTESIAN_POINT('Origin',(25.,-6.25103652921323,0.));
#3094=CARTESIAN_POINT('Origin',(26.8,-3.98983552758699,0.2));
#3095=CARTESIAN_POINT('',(26.6,6.25103652921323,0.));
#3096=CARTESIAN_POINT('',(26.6,6.25103652921323,0.));
#3097=CARTESIAN_POINT('',(26.6,-3.98983552758699,0.));
#3098=CARTESIAN_POINT('Origin',(25.,6.25103652921323,0.2));
#3099=CARTESIAN_POINT('',(25.2912820512821,7.82429898875421,0.));
#3100=CARTESIAN_POINT('',(25.3641025641026,8.21761460363946,0.4));
#3101=CARTESIAN_POINT('',(25.2912820512821,7.82429898875421,0.));
#3102=CARTESIAN_POINT('Origin',(25.,6.25103652921323,0.4));
#3103=CARTESIAN_POINT('Origin',(25.,6.25103652921323,0.));
#3104=CARTESIAN_POINT('Origin',(29.26,29.26,0.2));
#3105=CARTESIAN_POINT('',(7.82429898875421,25.2912820512821,0.));
#3106=CARTESIAN_POINT('Origin',(29.26,29.26,0.));
#3107=CARTESIAN_POINT('',(8.21761460363946,25.3641025641026,0.4));
#3108=CARTESIAN_POINT('',(7.82429898875421,25.2912820512821,0.));
#3109=CARTESIAN_POINT('Origin',(29.26,29.26,0.4));
#3110=CARTESIAN_POINT('Origin',(6.25103652921323,25.,0.2));
#3111=CARTESIAN_POINT('',(6.25103652921323,26.6,0.));
#3112=CARTESIAN_POINT('',(6.25103652921323,26.6,0.));
#3113=CARTESIAN_POINT('Origin',(6.25103652921323,25.,0.4));
#3114=CARTESIAN_POINT('Origin',(6.25103652921323,25.,0.));
#3115=CARTESIAN_POINT('Origin',(3.98983552758699,26.8,0.2));
#3116=CARTESIAN_POINT('',(-6.25103652921323,26.6,0.));
#3117=CARTESIAN_POINT('',(-6.25103652921323,26.6,0.));
#3118=CARTESIAN_POINT('',(3.98983552758699,26.6,0.));
#3119=CARTESIAN_POINT('Origin',(-6.25103652921323,25.,0.2));
#3120=CARTESIAN_POINT('',(-7.8242989887542,25.2912820512821,0.));
#3121=CARTESIAN_POINT('',(-8.21761460363945,25.3641025641026,0.4));
#3122=CARTESIAN_POINT('',(-7.8242989887542,25.2912820512821,0.));
#3123=CARTESIAN_POINT('Origin',(-6.25103652921323,25.,0.4));
#3124=CARTESIAN_POINT('Origin',(-6.25103652921323,25.,0.));
#3125=CARTESIAN_POINT('Origin',(-29.26,29.26,0.2));
#3126=CARTESIAN_POINT('',(-25.2912820512821,7.82429898875421,0.));
#3127=CARTESIAN_POINT('Origin',(-29.26,29.26,0.));
#3128=CARTESIAN_POINT('',(-25.3641025641026,8.21761460363946,0.4));
#3129=CARTESIAN_POINT('',(-25.2912820512821,7.82429898875421,0.));
#3130=CARTESIAN_POINT('Origin',(-29.26,29.26,0.4));
#3131=CARTESIAN_POINT('Origin',(-25.,6.25103652921323,0.2));
#3132=CARTESIAN_POINT('',(-26.6,6.25103652921323,0.));
#3133=CARTESIAN_POINT('',(-26.6,6.25103652921323,0.));
#3134=CARTESIAN_POINT('Origin',(-25.,6.25103652921323,0.4));
#3135=CARTESIAN_POINT('Origin',(-25.,6.25103652921323,0.));
#3136=CARTESIAN_POINT('Origin',(-26.8,3.98983552758699,0.2));
#3137=CARTESIAN_POINT('',(-26.6,-6.25103652921323,0.));
#3138=CARTESIAN_POINT('',(-26.6,-6.25103652921323,0.));
#3139=CARTESIAN_POINT('',(-26.6,3.98983552758699,0.));
#3140=CARTESIAN_POINT('Origin',(-25.,-6.25103652921323,0.2));
#3141=CARTESIAN_POINT('',(-25.2912820512821,-7.82429898875421,0.));
#3142=CARTESIAN_POINT('',(-25.3641025641026,-8.21761460363945,0.4));
#3143=CARTESIAN_POINT('',(-25.2912820512821,-7.82429898875421,0.));
#3144=CARTESIAN_POINT('Origin',(-25.,-6.25103652921323,0.4));
#3145=CARTESIAN_POINT('Origin',(-25.,-6.25103652921323,0.));
#3146=CARTESIAN_POINT('Origin',(-29.26,-29.26,0.2));
#3147=CARTESIAN_POINT('',(-7.82429898875422,-25.2912820512821,0.));
#3148=CARTESIAN_POINT('Origin',(-29.26,-29.26,0.));
#3149=CARTESIAN_POINT('',(-8.21761460363946,-25.3641025641026,0.4));
#3150=CARTESIAN_POINT('',(-7.82429898875422,-25.2912820512821,0.));
#3151=CARTESIAN_POINT('Origin',(-29.26,-29.26,0.4));
#3152=CARTESIAN_POINT('Origin',(-6.25103652921324,-25.,0.2));
#3153=CARTESIAN_POINT('Origin',(-6.25103652921324,-25.,0.4));
#3154=CARTESIAN_POINT('Origin',(-6.25103652921324,-25.,0.));
#3155=CARTESIAN_POINT('Origin',(-6.25103652921323,25.,0.));
#3156=CARTESIAN_POINT('',(-8.21761460363945,25.3641025641026,8.2));
#3157=CARTESIAN_POINT('',(-8.21761460363945,25.3641025641026,0.));
#3158=CARTESIAN_POINT('Origin',(-6.25103652921323,25.,8.2));
#3159=CARTESIAN_POINT('Origin',(-29.26,29.26,0.));
#3160=CARTESIAN_POINT('',(-25.3641025641026,8.21761460363946,8.2));
#3161=CARTESIAN_POINT('',(-25.3641025641026,8.21761460363946,0.));
#3162=CARTESIAN_POINT('Origin',(-29.26,29.26,8.2));
#3163=CARTESIAN_POINT('Origin',(-25.,6.25103652921323,0.));
#3164=CARTESIAN_POINT('Origin',(-25.,6.25103652921323,8.2));
#3165=CARTESIAN_POINT('Origin',(-25.,-6.25103652921323,0.));
#3166=CARTESIAN_POINT('',(-25.3641025641026,-8.21761460363945,8.2));
#3167=CARTESIAN_POINT('',(-25.3641025641026,-8.21761460363945,0.));
#3168=CARTESIAN_POINT('Origin',(-25.,-6.25103652921323,8.2));
#3169=CARTESIAN_POINT('Origin',(-29.26,-29.26,0.));
#3170=CARTESIAN_POINT('',(-8.21761460363946,-25.3641025641026,8.2));
#3171=CARTESIAN_POINT('',(-8.21761460363946,-25.3641025641026,0.));
#3172=CARTESIAN_POINT('Origin',(-29.26,-29.26,8.2));
#3173=CARTESIAN_POINT('Origin',(-6.25103652921324,-25.,0.));
#3174=CARTESIAN_POINT('Origin',(-6.25103652921324,-25.,8.2));
#3175=CARTESIAN_POINT('Origin',(0.,0.,0.));
#3176=CARTESIAN_POINT('',(-13.9,1.70225905081482E-15,0.));
#3177=CARTESIAN_POINT('Origin',(0.,0.,0.));
#3178=CARTESIAN_POINT('Origin',(0.,0.,0.2));
#3179=CARTESIAN_POINT('',(-13.5,-1.65327317884893E-15,0.4));
#3180=CARTESIAN_POINT('Origin',(0.,0.,0.4));
#3181=CARTESIAN_POINT('',(-13.7,-1.67776611483187E-15,0.2));
#3182=CARTESIAN_POINT('Origin',(0.,0.,0.));
#3183=CARTESIAN_POINT('',(-13.5,1.65327317884893E-15,8.2));
#3184=CARTESIAN_POINT('Origin',(0.,0.,8.2));
#3185=CARTESIAN_POINT('',(-13.5,-1.65327317884893E-15,0.));
#3186=CARTESIAN_POINT('Origin',(0.,0.,8.6));
#3187=CARTESIAN_POINT('',(-14.3,-1.75124492278072E-15,9.));
#3188=CARTESIAN_POINT('Origin',(0.,0.,9.));
#3189=CARTESIAN_POINT('',(-13.9,-1.70225905081482E-15,8.6));
#3190=CARTESIAN_POINT('Origin',(0.,0.,9.));
#3191=CARTESIAN_POINT('',(-7.43098337386896,25.2184615384615,9.));
#3192=CARTESIAN_POINT('',(-6.25103652921323,26.2,9.));
#3193=CARTESIAN_POINT('Origin',(-6.25103652921323,25.,9.));
#3194=CARTESIAN_POINT('',(-25.2184615384615,7.43098337386897,9.));
#3195=CARTESIAN_POINT('Origin',(-29.26,29.26,9.));
#3196=CARTESIAN_POINT('',(-26.2,6.25103652921323,9.));
#3197=CARTESIAN_POINT('Origin',(-25.,6.25103652921323,9.));
#3198=CARTESIAN_POINT('',(-26.2,-6.25103652921323,9.));
#3199=CARTESIAN_POINT('',(-26.2,3.98983552758699,9.));
#3200=CARTESIAN_POINT('',(-25.2184615384615,-7.43098337386896,9.));
#3201=CARTESIAN_POINT('Origin',(-25.,-6.25103652921323,9.));
#3202=CARTESIAN_POINT('',(-7.43098337386897,-25.2184615384615,9.));
#3203=CARTESIAN_POINT('Origin',(-29.26,-29.26,9.));
#3204=CARTESIAN_POINT('',(-6.25103652921324,-26.2,9.));
#3205=CARTESIAN_POINT('Origin',(-6.25103652921324,-25.,9.));
#3206=CARTESIAN_POINT('',(6.25103652921323,-26.2,9.));
#3207=CARTESIAN_POINT('',(-3.98983552758699,-26.2,9.));
#3208=CARTESIAN_POINT('',(7.43098337386896,-25.2184615384615,9.));
#3209=CARTESIAN_POINT('Origin',(6.25103652921323,-25.,9.));
#3210=CARTESIAN_POINT('',(25.2184615384615,-7.43098337386896,9.));
#3211=CARTESIAN_POINT('Origin',(29.26,-29.26,9.));
#3212=CARTESIAN_POINT('',(26.2,-6.25103652921323,9.));
#3213=CARTESIAN_POINT('Origin',(25.,-6.25103652921323,9.));
#3214=CARTESIAN_POINT('',(26.2,6.25103652921323,9.));
#3215=CARTESIAN_POINT('',(26.2,-3.98983552758699,9.));
#3216=CARTESIAN_POINT('',(25.2184615384615,7.43098337386897,9.));
#3217=CARTESIAN_POINT('Origin',(25.,6.25103652921323,9.));
#3218=CARTESIAN_POINT('',(7.43098337386897,25.2184615384615,9.));
#3219=CARTESIAN_POINT('Origin',(29.26,29.26,9.));
#3220=CARTESIAN_POINT('',(6.25103652921323,26.2,9.));
#3221=CARTESIAN_POINT('Origin',(6.25103652921323,25.,9.));
#3222=CARTESIAN_POINT('',(3.98983552758699,26.2,9.));
#3223=CARTESIAN_POINT('Origin',(-6.25103652921323,25.,8.6));
#3224=CARTESIAN_POINT('',(-6.25103652921323,26.2,9.));
#3225=CARTESIAN_POINT('',(-8.21761460363945,25.3641025641026,8.2));
#3226=CARTESIAN_POINT('Origin',(3.98983552758699,26.6,8.6));
#3227=CARTESIAN_POINT('',(6.25103652921323,26.2,9.));
#3228=CARTESIAN_POINT('Origin',(6.25103652921323,25.,8.6));
#3229=CARTESIAN_POINT('',(8.21761460363946,25.3641025641026,8.2));
#3230=CARTESIAN_POINT('',(7.43098337386897,25.2184615384615,9.));
#3231=CARTESIAN_POINT('Origin',(6.25103652921323,25.,8.2));
#3232=CARTESIAN_POINT('Origin',(29.26,29.26,8.6));
#3233=CARTESIAN_POINT('',(25.3641025641026,8.21761460363946,8.2));
#3234=CARTESIAN_POINT('',(25.2184615384615,7.43098337386897,9.));
#3235=CARTESIAN_POINT('Origin',(29.26,29.26,8.2));
#3236=CARTESIAN_POINT('Origin',(25.,6.25103652921323,8.6));
#3237=CARTESIAN_POINT('',(26.2,6.25103652921323,9.));
#3238=CARTESIAN_POINT('Origin',(25.,6.25103652921323,8.2));
#3239=CARTESIAN_POINT('Origin',(26.6,-3.98983552758699,8.6));
#3240=CARTESIAN_POINT('',(26.2,-6.25103652921323,9.));
#3241=CARTESIAN_POINT('Origin',(25.,-6.25103652921323,8.6));
#3242=CARTESIAN_POINT('',(25.3641025641026,-8.21761460363945,8.2));
#3243=CARTESIAN_POINT('',(25.2184615384615,-7.43098337386896,9.));
#3244=CARTESIAN_POINT('Origin',(25.,-6.25103652921323,8.2));
#3245=CARTESIAN_POINT('Origin',(29.26,-29.26,8.6));
#3246=CARTESIAN_POINT('',(8.21761460363944,-25.3641025641026,8.2));
#3247=CARTESIAN_POINT('',(7.43098337386896,-25.2184615384615,9.));
#3248=CARTESIAN_POINT('Origin',(29.26,-29.26,8.2));
#3249=CARTESIAN_POINT('Origin',(6.25103652921323,-25.,8.6));
#3250=CARTESIAN_POINT('',(6.25103652921323,-26.2,9.));
#3251=CARTESIAN_POINT('Origin',(6.25103652921323,-25.,8.2));
#3252=CARTESIAN_POINT('Origin',(-3.98983552758699,-26.6,8.6));
#3253=CARTESIAN_POINT('',(-6.25103652921324,-26.2,9.));
#3254=CARTESIAN_POINT('Origin',(-6.25103652921324,-25.,8.6));
#3255=CARTESIAN_POINT('',(-7.43098337386897,-25.2184615384615,9.));
#3256=CARTESIAN_POINT('Origin',(-29.26,-29.26,8.6));
#3257=CARTESIAN_POINT('',(-25.2184615384615,-7.43098337386896,9.));
#3258=CARTESIAN_POINT('Origin',(-25.,-6.25103652921323,8.6));
#3259=CARTESIAN_POINT('',(-26.2,-6.25103652921323,9.));
#3260=CARTESIAN_POINT('Origin',(-26.6,3.98983552758699,8.6));
#3261=CARTESIAN_POINT('',(-26.2,6.25103652921323,9.));
#3262=CARTESIAN_POINT('Origin',(-25.,6.25103652921323,8.6));
#3263=CARTESIAN_POINT('',(-25.2184615384615,7.43098337386897,9.));
#3264=CARTESIAN_POINT('Origin',(-29.26,29.26,8.6));
#3265=CARTESIAN_POINT('Origin',(6.25103652921323,-25.,0.));
#3266=CARTESIAN_POINT('',(8.21761460363944,-25.3641025641026,0.));
#3267=CARTESIAN_POINT('Origin',(25.,-6.25103652921323,0.));
#3268=CARTESIAN_POINT('',(25.3641025641026,-8.21761460363945,0.));
#3269=CARTESIAN_POINT('Origin',(25.,6.25103652921323,0.));
#3270=CARTESIAN_POINT('',(25.3641025641026,8.21761460363946,0.));
#3271=CARTESIAN_POINT('Origin',(6.25103652921323,25.,0.));
#3272=CARTESIAN_POINT('',(8.21761460363946,25.3641025641026,0.));
#3273=CARTESIAN_POINT('Origin',(29.26,29.26,0.));
#3274=CARTESIAN_POINT('Origin',(29.26,-29.26,0.));
#3328=UNCERTAINTY_MEASURE_WITH_UNIT(LENGTH_MEASURE(0.01),#3339,
'DISTANCE_ACCURACY_VALUE',
'Maximum model space distance between geometric entities at asserted c
onnectivities');
#3332=UNCERTAINTY_MEASURE_WITH_UNIT(LENGTH_MEASURE(0.01),#3339,
'DISTANCE_ACCURACY_VALUE',
'Maximum model space distance between geometric entities at asserted c
onnectivities');
#3334=(
GEOMETRIC_REPRESENTATION_CONTEXT(3)
GLOBAL_UNCERTAINTY_ASSIGNED_CONTEXT((#3328))
GLOBAL_UNIT_ASSIGNED_CONTEXT((#3339,#3341,#3342))
REPRESENTATION_CONTEXT('','3D')
);
#3338=(
GEOMETRIC_REPRESENTATION_CONTEXT(3)
GLOBAL_UNCERTAINTY_ASSIGNED_CONTEXT((#3332))
GLOBAL_UNIT_ASSIGNED_CONTEXT((#3339,#3341,#3342))
REPRESENTATION_CONTEXT('','3D')
);
#3339=(
LENGTH_UNIT()
NAMED_UNIT(*)
SI_UNIT(.MILLI.,.METRE.)
);
#3341=(
NAMED_UNIT(*)
PLANE_ANGLE_UNIT()
SI_UNIT($,.RADIAN.)
);
#3342=(
NAMED_UNIT(*)
SI_UNIT($,.STERADIAN.)
SOLID_ANGLE_UNIT()
);
#3344=SHAPE_DEFINITION_REPRESENTATION(#3349,#3367);
#3349=PRODUCT_DEFINITION_SHAPE('',$,#3373);
#3367=SHAPE_REPRESENTATION('',(#1624),#3334);
#3371=PRODUCT_DEFINITION_CONTEXT('part definition',#3388,'design');
#3373=PRODUCT_DEFINITION('2026-10-11-08-53-15-906',
'01_Coupler_Body_CNC_6061',#3378,#3371);
#3378=PRODUCT_DEFINITION_FORMATION('',$,#3391);
#3388=APPLICATION_CONTEXT(
'Core Data for Automotive Mechanical Design Process');
#3389=PRODUCT_CONTEXT('part definition',#3388,'mechanical');
#3391=PRODUCT('2026-10-11-08-53-15-906','01_Coupler_Body_CNC_6061',$,(#3389));
#3430=COLOUR_RGB('Dark Blue',0.08,0.2,0.34);
#3431=FILL_AREA_STYLE_COLOUR('',#3430);
#3432=FILL_AREA_STYLE('',(#3431));
#3433=SURFACE_STYLE_FILL_AREA(#3432);
#3434=SURFACE_SIDE_STYLE('',(#3433));
#3435=SURFACE_STYLE_USAGE(.BOTH.,#3434);
#3436=PRESENTATION_STYLE_ASSIGNMENT((#3435));
ENDSEC;
END-ISO-10303-21;
